ISO-10303-21;
HEADER;
/* Generated by software containing ST-Developer
 * from STEP Tools, Inc. (www.steptools.com) 
 */

FILE_DESCRIPTION(
/* description */ (''),
/* implementation_level */ '2;1');

FILE_NAME(
/* name */ 'Spring.step',
/* time_stamp */ '2026-10-23T22:29:29+06:00',
/* author */ (''),
/* organization */ (''),
/* preprocessor_version */ 'ST-DEVELOPER v20.2',
/* originating_system */ 'Autodesk Translation Framework v15.15.0.0',
/* authorisation */ '');

FILE_SCHEMA (('AUTOMOTIVE_DESIGN { 1 0 10303 214 3 1 1 }'));
ENDSEC;

DATA;
#10=MECHANICAL_DESIGN_GEOMETRIC_PRESENTATION_REPRESENTATION('',(#80),#7047);
#51=B_SPLINE_SURFACE_WITH_KNOTS('',3,3,((#6062,#6063,#6064,#6065,#6066,
#6067,#6068,#6069,#6070,#6071,#6072,#6073,#6074,#6075,#6076,#6077,#6078,
#6079,#6080,#6081,#6082,#6083,#6084,#6085,#6086,#6087,#6088,#6089,#6090,
#6091,#6092,#6093,#6094,#6095,#6096,#6097,#6098,#6099,#6100,#6101,#6102,
#6103,#6104,#6105,#6106,#6107,#6108,#6109,#6110,#6111,#6112,#6113,#6114,
#6115,#6116,#6117,#6118,#6119,#6120,#6121,#6122,#6123,#6124,#6125,#6126,
#6127,#6128,#6129,#6130,#6131,#6132,#6133,#6134,#6135,#6136,#6137,#6138,
#6139,#6140),(#6141,#6142,#6143,#6144,#6145,#6146,#6147,#6148,#6149,#6150,
#6151,#6152,#6153,#6154,#6155,#6156,#6157,#6158,#6159,#6160,#6161,#6162,
#6163,#6164,#6165,#6166,#6167,#6168,#6169,#6170,#6171,#6172,#6173,#6174,
#6175,#6176,#6177,#6178,#6179,#6180,#6181,#6182,#6183,#6184,#6185,#6186,
#6187,#6188,#6189,#6190,#6191,#6192,#6193,#6194,#6195,#6196,#6197,#6198,
#6199,#6200,#6201,#6202,#6203,#6204,#6205,#6206,#6207,#6208,#6209,#6210,
#6211,#6212,#6213,#6214,#6215,#6216,#6217,#6218,#6219),(#6220,#6221,#6222,
#6223,#6224,#6225,#6226,#6227,#6228,#6229,#6230,#6231,#6232,#6233,#6234,
#6235,#6236,#6237,#6238,#6239,#6240,#6241,#6242,#6243,#6244,#6245,#6246,
#6247,#6248,#6249,#6250,#6251,#6252,#6253,#6254,#6255,#6256,#6257,#6258,
#6259,#6260,#6261,#6262,#6263,#6264,#6265,#6266,#6267,#6268,#6269,#6270,
#6271,#6272,#6273,#6274,#6275,#6276,#6277,#6278,#6279,#6280,#6281,#6282,
#6283,#6284,#6285,#6286,#6287,#6288,#6289,#6290,#6291,#6292,#6293,#6294,
#6295,#6296,#6297,#6298),(#6299,#6300,#6301,#6302,#6303,#6304,#6305,#6306,
#6307,#6308,#6309,#6310,#6311,#6312,#6313,#6314,#6315,#6316,#6317,#6318,
#6319,#6320,#6321,#6322,#6323,#6324,#6325,#6326,#6327,#6328,#6329,#6330,
#6331,#6332,#6333,#6334,#6335,#6336,#6337,#6338,#6339,#6340,#6341,#6342,
#6343,#6344,#6345,#6346,#6347,#6348,#6349,#6350,#6351,#6352,#6353,#6354,
#6355,#6356,#6357,#6358,#6359,#6360,#6361,#6362,#6363,#6364,#6365,#6366,
#6367,#6368,#6369,#6370,#6371,#6372,#6373,#6374,#6375,#6376,#6377),(#6378,
#6379,#6380,#6381,#6382,#6383,#6384,#6385,#6386,#6387,#6388,#6389,#6390,
#6391,#6392,#6393,#6394,#6395,#6396,#6397,#6398,#6399,#6400,#6401,#6402,
#6403,#6404,#6405,#6406,#6407,#6408,#6409,#6410,#6411,#6412,#6413,#6414,
#6415,#6416,#6417,#6418,#6419,#6420,#6421,#6422,#6423,#6424,#6425,#6426,
#6427,#6428,#6429,#6430,#6431,#6432,#6433,#6434,#6435,#6436,#6437,#6438,
#6439,#6440,#6441,#6442,#6443,#6444,#6445,#6446,#6447,#6448,#6449,#6450,
#6451,#6452,#6453,#6454,#6455,#6456),(#6457,#6458,#6459,#6460,#6461,#6462,
#6463,#6464,#6465,#6466,#6467,#6468,#6469,#6470,#6471,#6472,#6473,#6474,
#6475,#6476,#6477,#6478,#6479,#6480,#6481,#6482,#6483,#6484,#6485,#6486,
#6487,#6488,#6489,#6490,#6491,#6492,#6493,#6494,#6495,#6496,#6497,#6498,
#6499,#6500,#6501,#6502,#6503,#6504,#6505,#6506,#6507,#6508,#6509,#6510,
#6511,#6512,#6513,#6514,#6515,#6516,#6517,#6518,#6519,#6520,#6521,#6522,
#6523,#6524,#6525,#6526,#6527,#6528,#6529,#6530,#6531,#6532,#6533,#6534,
#6535),(#6536,#6537,#6538,#6539,#6540,#6541,#6542,#6543,#6544,#6545,#6546,
#6547,#6548,#6549,#6550,#6551,#6552,#6553,#6554,#6555,#6556,#6557,#6558,
#6559,#6560,#6561,#6562,#6563,#6564,#6565,#6566,#6567,#6568,#6569,#6570,
#6571,#6572,#6573,#6574,#6575,#6576,#6577,#6578,#6579,#6580,#6581,#6582,
#6583,#6584,#6585,#6586,#6587,#6588,#6589,#6590,#6591,#6592,#6593,#6594,
#6595,#6596,#6597,#6598,#6599,#6600,#6601,#6602,#6603,#6604,#6605,#6606,
#6607,#6608,#6609,#6610,#6611,#6612,#6613,#6614),(#6615,#6616,#6617,#6618,
#6619,#6620,#6621,#6622,#6623,#6624,#6625,#6626,#6627,#6628,#6629,#6630,
#6631,#6632,#6633,#6634,#6635,#6636,#6637,#6638,#6639,#6640,#6641,#6642,
#6643,#6644,#6645,#6646,#6647,#6648,#6649,#6650,#6651,#6652,#6653,#6654,
#6655,#6656,#6657,#6658,#6659,#6660,#6661,#6662,#6663,#6664,#6665,#6666,
#6667,#6668,#6669,#6670,#6671,#6672,#6673,#6674,#6675,#6676,#6677,#6678,
#6679,#6680,#6681,#6682,#6683,#6684,#6685,#6686,#6687,#6688,#6689,#6690,
#6691,#6692,#6693),(#6694,#6695,#6696,#6697,#6698,#6699,#6700,#6701,#6702,
#6703,#6704,#6705,#6706,#6707,#6708,#6709,#6710,#6711,#6712,#6713,#6714,
#6715,#6716,#6717,#6718,#6719,#6720,#6721,#6722,#6723,#6724,#6725,#6726,
#6727,#6728,#6729,#6730,#6731,#6732,#6733,#6734,#6735,#6736,#6737,#6738,
#6739,#6740,#6741,#6742,#6743,#6744,#6745,#6746,#6747,#6748,#6749,#6750,
#6751,#6752,#6753,#6754,#6755,#6756,#6757,#6758,#6759,#6760,#6761,#6762,
#6763,#6764,#6765,#6766,#6767,#6768,#6769,#6770,#6771,#6772),(#6773,#6774,
#6775,#6776,#6777,#6778,#6779,#6780,#6781,#6782,#6783,#6784,#6785,#6786,
#6787,#6788,#6789,#6790,#6791,#6792,#6793,#6794,#6795,#6796,#6797,#6798,
#6799,#6800,#6801,#6802,#6803,#6804,#6805,#6806,#6807,#6808,#6809,#6810,
#6811,#6812,#6813,#6814,#6815,#6816,#6817,#6818,#6819,#6820,#6821,#6822,
#6823,#6824,#6825,#6826,#6827,#6828,#6829,#6830,#6831,#6832,#6833,#6834,
#6835,#6836,#6837,#6838,#6839,#6840,#6841,#6842,#6843,#6844,#6845,#6846,
#6847,#6848,#6849,#6850,#6851)),.UNSPECIFIED.,.T.,.F.,.F.,(4,1,1,1,1,1,
1,4),(4,1,1,1,1,1,1,1,1,1,1,1,1,1,1,1,1,1,1,1,1,1,1,1,1,1,1,1,1,1,1,1,1,
1,1,1,1,1,1,1,1,1,1,1,1,1,1,1,1,1,1,1,1,1,1,1,1,1,1,1,1,1,1,1,1,1,1,1,1,
1,1,1,1,1,1,1,4),(-3.14159265358979,-2.24399475256414,-1.34639685153848,
-0.448798950512828,0.448798950512828,1.34639685153848,2.24399475256414,
3.14159265358979),(0.,0.496040945303652,0.992081890607303,1.48812283591095,
1.98416378121461,2.48020472651826,2.97624567182191,3.47228661712556,3.96832756242921,
4.46436850773286,4.96040945303652,5.45645039834017,5.95249134364382,6.44853228894747,
6.94457323425112,7.44061417955477,7.93665512485842,8.43269607016208,8.92873701546573,
9.42477796076938,9.92081890607303,10.4168598513767,10.9129007966803,11.408941741984,
11.9049826872876,12.4010236325913,12.8970645778949,13.3931055231986,13.8891464685022,
14.3851874138059,14.8812283591095,15.3772693044132,15.8733102497168,16.3693511950205,
16.8653921403242,17.3614330856278,17.8574740309315,18.3535149762351,18.8495559215388,
19.3455968668424,19.8416378121461,20.3376787574497,20.8337197027534,21.329760648057,
21.8258015933607,22.3218425386643,22.817883483968,23.3139244292716,23.8099653745753,
24.3060063198789,24.8020472651826,25.2980882104862,25.7941291557899,26.2901701010935,
26.7862110463972,27.2822519917008,27.7782929370045,28.2743338823081,28.7703748276118,
29.2664157729154,29.7624567182191,30.2584976635227,30.7545386088264,31.25057955413,
31.7466204994337,32.2426614447374,32.738702390041,33.2347433353447,33.7307842806483,
34.226825225952,34.7228661712556,35.2189071165593,35.7149480618629,36.2109890071666,
36.7070299524702,37.2030708977739,37.6991118430775),.UNSPECIFIED.);
#60=SHAPE_REPRESENTATION_RELATIONSHIP('SRR','None',#7093,#70);
#70=ADVANCED_BREP_SHAPE_REPRESENTATION('',(#93),#7045);
#80=STYLED_ITEM('',(#7198),#93);
#93=MANIFOLD_SOLID_BREP('Spring',#3405);
#248=PLANE('',#3863);
#249=PLANE('',#3864);
#436=FACE_OUTER_BOUND('',#641,.T.);
#437=FACE_OUTER_BOUND('',#642,.T.);
#438=FACE_OUTER_BOUND('',#643,.T.);
#641=EDGE_LOOP('',(#3095,#3096,#3097,#3098));
#642=EDGE_LOOP('',(#3099));
#643=EDGE_LOOP('',(#3100));
#793=CIRCLE('',#3861,1.);
#794=CIRCLE('',#3862,1.);
#1431=B_SPLINE_CURVE_WITH_KNOTS('',3,(#6855,#6856,#6857,#6858,#6859,#6860,
#6861,#6862,#6863,#6864,#6865,#6866,#6867,#6868,#6869,#6870,#6871,#6872,
#6873,#6874,#6875,#6876,#6877,#6878,#6879,#6880,#6881,#6882,#6883,#6884,
#6885,#6886,#6887,#6888,#6889,#6890,#6891,#6892,#6893,#6894,#6895,#6896,
#6897,#6898,#6899,#6900,#6901,#6902,#6903,#6904,#6905,#6906,#6907,#6908,
#6909,#6910,#6911,#6912,#6913,#6914,#6915,#6916,#6917,#6918,#6919,#6920,
#6921,#6922,#6923,#6924,#6925,#6926,#6927,#6928,#6929,#6930,#6931,#6932,
#6933),.UNSPECIFIED.,.F.,.F.,(4,1,1,1,1,1,1,1,1,1,1,1,1,1,1,1,1,1,1,1,1,
1,1,1,1,1,1,1,1,1,1,1,1,1,1,1,1,1,1,1,1,1,1,1,1,1,1,1,1,1,1,1,1,1,1,1,1,
1,1,1,1,1,1,1,1,1,1,1,1,1,1,1,1,1,1,1,4),(0.,0.496040945303652,0.992081890607303,
1.48812283591095,1.98416378121461,2.48020472651826,2.97624567182191,3.47228661712556,
3.96832756242921,4.46436850773286,4.96040945303652,5.45645039834017,5.95249134364382,
6.44853228894747,6.94457323425112,7.44061417955477,7.93665512485842,8.43269607016208,
8.92873701546573,9.42477796076938,9.92081890607303,10.4168598513767,10.9129007966803,
11.408941741984,11.9049826872876,12.4010236325913,12.8970645778949,13.3931055231986,
13.8891464685022,14.3851874138059,14.8812283591095,15.3772693044132,15.8733102497168,
16.3693511950205,16.8653921403242,17.3614330856278,17.8574740309315,18.3535149762351,
18.8495559215388,19.3455968668424,19.8416378121461,20.3376787574497,20.8337197027534,
21.329760648057,21.8258015933607,22.3218425386643,22.817883483968,23.3139244292716,
23.8099653745753,24.3060063198789,24.8020472651826,25.2980882104862,25.7941291557899,
26.2901701010935,26.7862110463972,27.2822519917008,27.7782929370045,28.2743338823081,
28.7703748276118,29.2664157729154,29.7624567182191,30.2584976635227,30.7545386088264,
31.25057955413,31.7466204994337,32.2426614447374,32.738702390041,33.2347433353447,
33.7307842806483,34.226825225952,34.7228661712556,35.2189071165593,35.7149480618629,
36.2109890071666,36.7070299524702,37.2030708977739,37.6991118430775),
 .UNSPECIFIED.);
#1719=VERTEX_POINT('',#6852);
#1720=VERTEX_POINT('',#6854);
#2182=EDGE_CURVE('',#1719,#1719,#793,.T.);
#2183=EDGE_CURVE('',#1719,#1720,#1431,.T.);
#2184=EDGE_CURVE('',#1720,#1720,#794,.T.);
#3095=ORIENTED_EDGE('',*,*,#2182,.T.);
#3096=ORIENTED_EDGE('',*,*,#2183,.T.);
#3097=ORIENTED_EDGE('',*,*,#2184,.F.);
#3098=ORIENTED_EDGE('',*,*,#2183,.F.);
#3099=ORIENTED_EDGE('',*,*,#2184,.T.);
#3100=ORIENTED_EDGE('',*,*,#2182,.F.);
#3378=ADVANCED_FACE('',(#436),#51,.T.);
#3379=ADVANCED_FACE('',(#437),#248,.T.);
#3380=ADVANCED_FACE('',(#438),#249,.F.);
#3405=CLOSED_SHELL('',(#3378,#3379,#3380));
#3860=AXIS2_PLACEMENT_3D('',#6061,#4834,#4835);
#3861=AXIS2_PLACEMENT_3D('',#6853,#4836,#4837);
#3862=AXIS2_PLACEMENT_3D('',#6934,#4838,#4839);
#3863=AXIS2_PLACEMENT_3D('',#6935,#4840,#4841);
#3864=AXIS2_PLACEMENT_3D('',#6936,#4842,#4843);
#4834=DIRECTION('axis',(0.,0.,1.));
#4835=DIRECTION('refdir',(1.,0.,0.));
#4836=DIRECTION('center_axis',(0.,0.,1.));
#4837=DIRECTION('ref_axis',(1.,0.,0.));
#4838=DIRECTION('center_axis',(0.,1.46957615897682E-15,1.));
#4839=DIRECTION('ref_axis',(1.,0.,0.));
#4840=DIRECTION('center_axis',(0.,1.46957615897682E-15,1.));
#4841=DIRECTION('ref_axis',(1.,0.,0.));
#4842=DIRECTION('center_axis',(0.,0.,1.));
#4843=DIRECTION('ref_axis',(1.,0.,0.));
#6061=CARTESIAN_POINT('',(0.,0.,0.));
#6062=CARTESIAN_POINT('Ctrl Pts',(-21.,11.5223833765015,10.2662081021742));
#6063=CARTESIAN_POINT('Ctrl Pts',(-20.8245614035088,11.5223833765015,11.0929430110137));
#6064=CARTESIAN_POINT('Ctrl Pts',(-20.4736842105263,11.1043754458166,12.7456006386873));
#6065=CARTESIAN_POINT('Ctrl Pts',(-19.9473684210526,9.37174604195822,14.627693070812));
#6066=CARTESIAN_POINT('Ctrl Pts',(-19.421052631579,6.95264079877442,15.4581010648004));
#6067=CARTESIAN_POINT('Ctrl Pts',(-18.8947368421052,4.4296403847971,15.0371536204255));
#6068=CARTESIAN_POINT('Ctrl Pts',(-18.3684210526316,2.41118846113653,13.4660782459265));
#6069=CARTESIAN_POINT('Ctrl Pts',(-17.8421052631579,1.38370759752575,11.1237050325294));
#6070=CARTESIAN_POINT('Ctrl Pts',(-17.3157894736842,1.59493822839275,8.57461107686665));
#6071=CARTESIAN_POINT('Ctrl Pts',(-16.7894736842105,2.9939316339387,6.43329006745293));
#6072=CARTESIAN_POINT('Ctrl Pts',(-16.2631578947368,5.2434721166514,5.21589900368628));
#6073=CARTESIAN_POINT('Ctrl Pts',(-15.7368421052632,7.80129492555693,5.21589976806491));
#6074=CARTESIAN_POINT('Ctrl Pts',(-15.2105263157895,10.0508340962501,6.43328889288153));
#6075=CARTESIAN_POINT('Ctrl Pts',(-14.6842105263158,11.4498308299117,8.57461329194773));
#6076=CARTESIAN_POINT('Ctrl Pts',(-14.1578947368421,11.6610543305691,11.1237005882441));
#6077=CARTESIAN_POINT('Ctrl Pts',(-13.6315789473684,10.6335882256263,13.4660873044149));
#6078=CARTESIAN_POINT('Ctrl Pts',(-13.1052631578947,8.61510599100168,15.0371350857393));
#6079=CARTESIAN_POINT('Ctrl Pts',(-12.5789473684211,6.09216771054517,15.4581390317312));
#6080=CARTESIAN_POINT('Ctrl Pts',(-12.0526315789474,3.67293400690476,14.6276150452767));
#6081=CARTESIAN_POINT('Ctrl Pts',(-11.5263157894737,1.94056718272496,12.7457630293102));
#6082=CARTESIAN_POINT('Ctrl Pts',(-11.,1.31265859936127,10.2662081017794));
#6083=CARTESIAN_POINT('Ctrl Pts',(-10.4736842105263,1.9405671834026,7.78665317603972));
#6084=CARTESIAN_POINT('Ctrl Pts',(-9.94736842105264,3.67293400518582,5.90480115732107));
#6085=CARTESIAN_POINT('Ctrl Pts',(-9.42105263157895,6.09216771422783,5.07427717605678));
#6086=CARTESIAN_POINT('Ctrl Pts',(-8.89473684210527,8.61510598337903,5.49528111163513));
#6087=CARTESIAN_POINT('Ctrl Pts',(-8.36842105263158,10.6335882412796,7.06632891418456));
#6088=CARTESIAN_POINT('Ctrl Pts',(-7.84210526315789,11.6610542984852,9.40871558692863));
#6089=CARTESIAN_POINT('Ctrl Pts',(-7.31578947368422,11.4498308956436,11.9578029721578));
#6090=CARTESIAN_POINT('Ctrl Pts',(-6.78947368421053,10.0508339615961,14.0991271890608));
#6091=CARTESIAN_POINT('Ctrl Pts',(-6.26315789473684,7.80129520139315,15.3165166870263));
#6092=CARTESIAN_POINT('Ctrl Pts',(-5.73684210526316,5.24347155160944,15.3165166870254));
#6093=CARTESIAN_POINT('Ctrl Pts',(-5.21052631578947,2.99393279140807,14.0991271890622));
#6094=CARTESIAN_POINT('Ctrl Pts',(-4.68421052631579,1.59493585735657,11.9578029721551));
#6095=CARTESIAN_POINT('Ctrl Pts',(-4.15789473684211,1.38371245452358,9.408715586934));
#6096=CARTESIAN_POINT('Ctrl Pts',(-3.63157894736843,2.41117851171133,7.0663289141736));
#6097=CARTESIAN_POINT('Ctrl Pts',(-3.10526315789474,4.42966076964857,5.49528111165755));
#6098=CARTESIAN_POINT('Ctrl Pts',(-2.57894736842106,6.95259903872457,5.07427717601085));
#6099=CARTESIAN_POINT('Ctrl Pts',(-2.05263157894737,9.3718327479206,5.90480115741515));
#6100=CARTESIAN_POINT('Ctrl Pts',(-1.52631578947369,11.1041995693883,7.78665317584699));
#6101=CARTESIAN_POINT('Ctrl Pts',(-1.,11.732108154076,10.2662081021742));
#6102=CARTESIAN_POINT('Ctrl Pts',(-0.47368421052632,11.1041995693883,12.7457630285015));
#6103=CARTESIAN_POINT('Ctrl Pts',(0.052631578947363,9.37183274792061,14.6276150469333));
#6104=CARTESIAN_POINT('Ctrl Pts',(0.578947368421052,6.95259903872456,15.4581390283376));
#6105=CARTESIAN_POINT('Ctrl Pts',(1.10526315789473,4.42966076964857,15.0371350926909));
#6106=CARTESIAN_POINT('Ctrl Pts',(1.63157894736842,2.41117851171132,13.4660872901749));
#6107=CARTESIAN_POINT('Ctrl Pts',(2.1578947368421,1.38371245452358,11.1237006174145));
#6108=CARTESIAN_POINT('Ctrl Pts',(2.68421052631579,1.59493585735657,8.57461323219337));
#6109=CARTESIAN_POINT('Ctrl Pts',(3.21052631578947,2.99393279140808,6.43328901528626));
#6110=CARTESIAN_POINT('Ctrl Pts',(3.73684210526315,5.24347155160942,5.21589951732309));
#6111=CARTESIAN_POINT('Ctrl Pts',(4.26315789473684,7.80129520139315,5.21589951732216));
#6112=CARTESIAN_POINT('Ctrl Pts',(4.78947368421052,10.0508339615961,6.43328901528768));
#6113=CARTESIAN_POINT('Ctrl Pts',(5.31578947368421,11.4498308956436,8.57461323219068));
#6114=CARTESIAN_POINT('Ctrl Pts',(5.84210526315788,11.6610542984852,11.1237006174198));
#6115=CARTESIAN_POINT('Ctrl Pts',(6.36842105263158,10.6335882412796,13.4660872901639));
#6116=CARTESIAN_POINT('Ctrl Pts',(6.89473684210526,8.61510598337902,15.0371350927133));
#6117=CARTESIAN_POINT('Ctrl Pts',(7.42105263157895,6.09216771422785,15.4581390282917));
#6118=CARTESIAN_POINT('Ctrl Pts',(7.94736842105263,3.67293400518582,14.6276150470274));
#6119=CARTESIAN_POINT('Ctrl Pts',(8.47368421052631,1.94056718340261,12.7457630283087));
#6120=CARTESIAN_POINT('Ctrl Pts',(9.,1.31265859936126,10.266208102569));
#6121=CARTESIAN_POINT('Ctrl Pts',(9.52631578947368,1.94056718272496,7.78665317503828));
#6122=CARTESIAN_POINT('Ctrl Pts',(10.0526315789474,3.67293400690476,5.90480115907178));
#6123=CARTESIAN_POINT('Ctrl Pts',(10.578947368421,6.09216771054518,5.07427717261729));
#6124=CARTESIAN_POINT('Ctrl Pts',(11.1052631578947,8.61510599100168,5.49528111860915));
#6125=CARTESIAN_POINT('Ctrl Pts',(11.6315789473684,10.6335882256264,7.06632889993352));
#6126=CARTESIAN_POINT('Ctrl Pts',(12.1578947368421,11.6610543305691,9.40871561610432));
#6127=CARTESIAN_POINT('Ctrl Pts',(12.6842105263158,11.4498308299117,11.9578029124007));
#6128=CARTESIAN_POINT('Ctrl Pts',(13.2105263157895,10.0508340962501,14.0991273114669));
#6129=CARTESIAN_POINT('Ctrl Pts',(13.7368421052632,7.80129492555691,15.3165164362836));
#6130=CARTESIAN_POINT('Ctrl Pts',(14.2631578947369,5.24347211665139,15.3165172006622));
#6131=CARTESIAN_POINT('Ctrl Pts',(14.7894736842105,2.9939316339387,14.0991261368955));
#6132=CARTESIAN_POINT('Ctrl Pts',(15.3157894736842,1.59493822839275,11.9578051274818));
#6133=CARTESIAN_POINT('Ctrl Pts',(15.8421052631579,1.38370759752574,9.4087111718191));
#6134=CARTESIAN_POINT('Ctrl Pts',(16.3684210526316,2.41118846113653,7.06633795842197));
#6135=CARTESIAN_POINT('Ctrl Pts',(16.8947368421052,4.42964038479711,5.49526258392294));
#6136=CARTESIAN_POINT('Ctrl Pts',(17.421052631579,6.95264079877441,5.07431513954803));
#6137=CARTESIAN_POINT('Ctrl Pts',(17.9473684210526,9.37174604195823,5.90472313353644));
#6138=CARTESIAN_POINT('Ctrl Pts',(18.4736842105263,11.1043754458165,7.78681556566119));
#6139=CARTESIAN_POINT('Ctrl Pts',(18.8245614035088,11.5223833765015,9.43947319333481));
#6140=CARTESIAN_POINT('Ctrl Pts',(19.,11.5223833765015,10.2662081021742));
#6141=CARTESIAN_POINT('Ctrl Pts',(-21.,11.2231840761596,10.2662081021742));
#6142=CARTESIAN_POINT('Ctrl Pts',(-20.8245614035088,11.2231840761596,11.0435502111341));
#6143=CARTESIAN_POINT('Ctrl Pts',(-20.4736842105263,10.8302077771026,12.5971984651315));
#6144=CARTESIAN_POINT('Ctrl Pts',(-19.9473684210526,9.20124552415081,14.3667344370862));
#6145=CARTESIAN_POINT('Ctrl Pts',(-19.421052631579,6.92689676613498,15.1474232419311));
#6146=CARTESIAN_POINT('Ctrl Pts',(-18.8947368421052,4.5548634960706,14.7516786250889));
#6147=CARTESIAN_POINT('Ctrl Pts',(-18.3684210526316,2.65719094980127,13.2746048239391));
#6148=CARTESIAN_POINT('Ctrl Pts',(-17.8421052631579,1.69119113188947,11.0723959995552));
#6149=CARTESIAN_POINT('Ctrl Pts',(-17.3157894736842,1.88978255726589,8.67583085991063));
#6150=CARTESIAN_POINT('Ctrl Pts',(-16.7894736842105,3.20506407724957,6.6626412124837));
#6151=CARTESIAN_POINT('Ctrl Pts',(-16.2631578947368,5.31999853405079,5.51809495225076));
#6152=CARTESIAN_POINT('Ctrl Pts',(-15.7368421052632,7.72476850015569,5.51809586750696));
#6153=CARTESIAN_POINT('Ctrl Pts',(-15.2105263157895,9.83970168123886,6.66263980606847));
#6154=CARTESIAN_POINT('Ctrl Pts',(-14.6842105263158,11.1549864372545,8.67583351221754));
#6155=CARTESIAN_POINT('Ctrl Pts',(-14.1578947368421,11.3535709297029,11.0723906780295));
#6156=CARTESIAN_POINT('Ctrl Pts',(-13.6315789473684,10.3875854621103,13.2746156704571));
#6157=CARTESIAN_POINT('Ctrl Pts',(-13.1052631578947,8.48988344353287,14.751656431547));
#6158=CARTESIAN_POINT('Ctrl Pts',(-12.5789473684211,6.11791058785403,15.1474687057993));
#6159=CARTESIAN_POINT('Ctrl Pts',(-12.0526315789474,3.84343692367721,14.36664090272));
#6160=CARTESIAN_POINT('Ctrl Pts',(-11.5263157894737,2.21472998524374,12.5973935404023));
#6161=CARTESIAN_POINT('Ctrl Pts',(-11.,1.62439365922802,10.2662081017015));
#6162=CARTESIAN_POINT('Ctrl Pts',(-10.4736842105263,2.21472998590263,7.93502266514533));
#6163=CARTESIAN_POINT('Ctrl Pts',(-9.94736842105264,3.84343692200583,6.16577529953216));
#6164=CARTESIAN_POINT('Ctrl Pts',(-9.42105263157895,6.11791059143481,5.38494750266754));
#6165=CARTESIAN_POINT('Ctrl Pts',(-8.89473684210527,8.48988343612111,5.78075976445089));
#6166=CARTESIAN_POINT('Ctrl Pts',(-8.36842105263158,10.3875854773305,7.25780055095535));
#6167=CARTESIAN_POINT('Ctrl Pts',(-7.84210526315789,11.3535708985067,9.46002549138446));
#6168=CARTESIAN_POINT('Ctrl Pts',(-7.31578947368422,11.1549865011677,11.8565827636832));
#6169=CARTESIAN_POINT('Ctrl Pts',(-6.78947368421053,9.83970155031053,13.8697762517126));
#6170=CARTESIAN_POINT('Ctrl Pts',(-6.26315789473684,7.72476876835996,15.0143206370773));
#6171=CARTESIAN_POINT('Ctrl Pts',(-5.73684210526316,5.31999798464263,15.0143206370762));
#6172=CARTESIAN_POINT('Ctrl Pts',(-5.21052631578947,3.20506520269362,13.8697762517143));
#6173=CARTESIAN_POINT('Ctrl Pts',(-4.68421052631579,1.88978025183249,11.8565827636799));
#6174=CARTESIAN_POINT('Ctrl Pts',(-4.15789473684211,1.69119585450193,9.4600254913909));
#6175=CARTESIAN_POINT('Ctrl Pts',(-3.63157894736843,2.65718127566077,7.25780055094221));
#6176=CARTESIAN_POINT('Ctrl Pts',(-3.10526315789474,4.55488331690579,5.78075976447775));
#6177=CARTESIAN_POINT('Ctrl Pts',(-2.57894736842106,6.926856161519,5.38494750261254));
#6178=CARTESIAN_POINT('Ctrl Pts',(-2.05263157894737,9.20132983109773,6.16577529964482));
#6179=CARTESIAN_POINT('Ctrl Pts',(-1.52631578947369,10.8300367668942,7.93502266491455));
#6180=CARTESIAN_POINT('Ctrl Pts',(-1.,11.4203730941972,10.2662081021742));
#6181=CARTESIAN_POINT('Ctrl Pts',(-0.47368421052632,10.8300367668942,12.5973935394339));
#6182=CARTESIAN_POINT('Ctrl Pts',(0.052631578947363,9.20132983109773,14.3666409047036));
#6183=CARTESIAN_POINT('Ctrl Pts',(0.578947368421052,6.92685616151899,15.1474687017359));
#6184=CARTESIAN_POINT('Ctrl Pts',(1.10526315789473,4.55488331690579,14.7516564398707));
#6185=CARTESIAN_POINT('Ctrl Pts',(1.63157894736842,2.65718127566077,13.2746156534063));
#6186=CARTESIAN_POINT('Ctrl Pts',(2.1578947368421,1.69119585450193,11.0723907129576));
#6187=CARTESIAN_POINT('Ctrl Pts',(2.68421052631579,1.88978025183249,8.67583344066851));
#6188=CARTESIAN_POINT('Ctrl Pts',(3.21052631578947,3.20506520269362,6.66263995263416));
#6189=CARTESIAN_POINT('Ctrl Pts',(3.73684210526315,5.31999798464262,5.51809556727224));
#6190=CARTESIAN_POINT('Ctrl Pts',(4.26315789473684,7.72476876835996,5.51809556727114));
#6191=CARTESIAN_POINT('Ctrl Pts',(4.78947368421052,9.83970155031051,6.66263995263585));
#6192=CARTESIAN_POINT('Ctrl Pts',(5.31578947368421,11.1549865011677,8.6758334406653));
#6193=CARTESIAN_POINT('Ctrl Pts',(5.84210526315788,11.3535708985067,11.072390712964));
#6194=CARTESIAN_POINT('Ctrl Pts',(6.36842105263158,10.3875854773305,13.2746156533931));
#6195=CARTESIAN_POINT('Ctrl Pts',(6.89473684210526,8.48988343612111,14.7516564398976));
#6196=CARTESIAN_POINT('Ctrl Pts',(7.42105263157895,6.11791059143481,15.1474687016809));
#6197=CARTESIAN_POINT('Ctrl Pts',(7.94736842105263,3.84343692200584,14.3666409048163));
#6198=CARTESIAN_POINT('Ctrl Pts',(8.47368421052631,2.21472998590264,12.5973935392031));
#6199=CARTESIAN_POINT('Ctrl Pts',(9.,1.62439365922802,10.266208102647));
#6200=CARTESIAN_POINT('Ctrl Pts',(9.52631578947368,2.21472998524374,7.9350226639462));
#6201=CARTESIAN_POINT('Ctrl Pts',(10.0526315789474,3.84343692367721,6.16577530162845));
#6202=CARTESIAN_POINT('Ctrl Pts',(10.578947368421,6.11791058785404,5.38494749854914));
#6203=CARTESIAN_POINT('Ctrl Pts',(11.1052631578947,8.48988344353287,5.78075977280148));
#6204=CARTESIAN_POINT('Ctrl Pts',(11.6315789473684,10.3875854621103,7.25780053389135));
#6205=CARTESIAN_POINT('Ctrl Pts',(12.1578947368421,11.3535709297029,9.460025526319));
#6206=CARTESIAN_POINT('Ctrl Pts',(12.6842105263158,11.1549864372545,11.8565826921309));
#6207=CARTESIAN_POINT('Ctrl Pts',(13.2105263157895,9.83970168123886,13.86977639828));
#6208=CARTESIAN_POINT('Ctrl Pts',(13.7368421052632,7.72476850015567,15.0143203368415));
#6209=CARTESIAN_POINT('Ctrl Pts',(14.2631578947369,5.31999853405078,15.0143212520977));
#6210=CARTESIAN_POINT('Ctrl Pts',(14.7894736842105,3.20506407724957,13.8697749918648));
#6211=CARTESIAN_POINT('Ctrl Pts',(15.3157894736842,1.88978255726589,11.8565853444378));
#6212=CARTESIAN_POINT('Ctrl Pts',(15.8421052631579,1.69119113188946,9.46002020479329));
#6213=CARTESIAN_POINT('Ctrl Pts',(16.3684210526316,2.65719094980128,7.25781138040935));
#6214=CARTESIAN_POINT('Ctrl Pts',(16.8947368421052,4.5548634960706,5.78073757925955));
#6215=CARTESIAN_POINT('Ctrl Pts',(17.421052631579,6.92689676613498,5.38499296241738));
#6216=CARTESIAN_POINT('Ctrl Pts',(17.9473684210526,9.20124552415082,6.16568176726222));
#6217=CARTESIAN_POINT('Ctrl Pts',(18.4736842105263,10.8302077771026,7.93521773921696));
#6218=CARTESIAN_POINT('Ctrl Pts',(18.8245614035088,11.2231840761596,9.48886599321435));
#6219=CARTESIAN_POINT('Ctrl Pts',(19.,11.2231840761596,10.2662081021742));
#6220=CARTESIAN_POINT('Ctrl Pts',(-20.7137377535255,10.6269009396766,10.2662081021742));
#6221=CARTESIAN_POINT('Ctrl Pts',(-20.5382991570343,10.6269009396766,10.945005547204));
#6222=CARTESIAN_POINT('Ctrl Pts',(-20.1874219640519,10.2837860836795,12.3014923419689));
#6223=CARTESIAN_POINT('Ctrl Pts',(-19.6611061745782,8.86144321099575,13.8466183137858));
#6224=CARTESIAN_POINT('Ctrl Pts',(-19.1347903851045,6.87558727517881,14.528258281606));
#6225=CARTESIAN_POINT('Ctrl Pts',(-18.6084745956308,4.80443303568469,14.182722745685));
#6226=CARTESIAN_POINT('Ctrl Pts',(-18.0821588061571,3.14747146421383,12.8930030485417));
#6227=CARTESIAN_POINT('Ctrl Pts',(-17.5558430166835,2.3040035227468,10.9701359564965));
#6228=CARTESIAN_POINT('Ctrl Pts',(-17.0295272272098,2.47740479551235,8.87756182299855));
#6229=CARTESIAN_POINT('Ctrl Pts',(-16.5032114377361,3.62584936605174,7.11973580265897));
#6230=CARTESIAN_POINT('Ctrl Pts',(-15.9768956482624,5.47251503489257,6.1203691946193));
#6231=CARTESIAN_POINT('Ctrl Pts',(-15.4505798587887,7.57225197059684,6.12037014070636));
#6232=CARTESIAN_POINT('Ctrl Pts',(-14.924264069315,9.41891649399846,7.11973434886793));
#6233=CARTESIAN_POINT('Ctrl Pts',(-14.3979482798413,10.5673639700999,8.87756456464978));
#6234=CARTESIAN_POINT('Ctrl Pts',(-13.8716324903676,10.7407590179416,10.9701304557117));
#6235=CARTESIAN_POINT('Ctrl Pts',(-13.345316700894,9.89730396131102,12.893014260437));
#6236=CARTESIAN_POINT('Ctrl Pts',(-12.8190009114203,8.2403159273021,14.1826998043253));
#6237=CARTESIAN_POINT('Ctrl Pts',(-12.2926851219466,6.16921593255766,14.528305278591));
#6238=CARTESIAN_POINT('Ctrl Pts',(-11.7663693324729,4.18324784624254,13.8465215654802));
#6239=CARTESIAN_POINT('Ctrl Pts',(-11.2400535429992,2.76113421485637,12.3016943587029));
#6240=CARTESIAN_POINT('Ctrl Pts',(-10.7137377535256,2.24567909126825,10.2662081016856));
#6241=CARTESIAN_POINT('Ctrl Pts',(-10.1874219640519,2.76113421544797,8.23072184688508));
#6242=CARTESIAN_POINT('Ctrl Pts',(-9.66110617457818,4.18324784474184,6.68589463670139));
#6243=CARTESIAN_POINT('Ctrl Pts',(-9.1347903851045,6.16921593577276,6.00411093001461));
#6244=CARTESIAN_POINT('Ctrl Pts',(-8.60847459563081,8.24031592064724,6.34971639139128));
#6245=CARTESIAN_POINT('Ctrl Pts',(-8.08215880615713,9.89730397497684,7.63940196155027));
#6246=CARTESIAN_POINT('Ctrl Pts',(-7.55584301668345,10.7407589899312,9.56228571252539));
#6247=CARTESIAN_POINT('Ctrl Pts',(-7.02952722720977,10.5673640274861,11.6548517136612));
#6248=CARTESIAN_POINT('Ctrl Pts',(-6.50321143773608,9.41891637644079,13.412681703976));
#6249=CARTESIAN_POINT('Ctrl Pts',(-5.9768956482624,7.57225221141156,14.4120463739915));
#6250=CARTESIAN_POINT('Ctrl Pts',(-5.45057985878871,5.47251454159106,14.4120463739904));
#6251=CARTESIAN_POINT('Ctrl Pts',(-4.92426406931503,3.62585037656322,13.4126817039777));
#6252=CARTESIAN_POINT('Ctrl Pts',(-4.39794827984135,2.47740272551435,11.6548517136579));
#6253=CARTESIAN_POINT('Ctrl Pts',(-3.87163249036766,2.30400776307679,9.56228571253205));
#6254=CARTESIAN_POINT('Ctrl Pts',(-3.34531670089398,3.14746277801559,7.6394019615367));
#6255=CARTESIAN_POINT('Ctrl Pts',(-2.81900091142029,4.80445083237722,6.34971639141904));
#6256=CARTESIAN_POINT('Ctrl Pts',(-2.29268512194661,6.87555081718607,6.00411092995776));
#6257=CARTESIAN_POINT('Ctrl Pts',(-1.76636933247292,8.86151890835144,6.68589463681784));
#6258=CARTESIAN_POINT('Ctrl Pts',(-1.24005354299924,10.2836325373699,8.23072184664655));
#6259=CARTESIAN_POINT('Ctrl Pts',(-0.713737753525556,10.7990876621138,10.2662081021742));
#6260=CARTESIAN_POINT('Ctrl Pts',(-0.187421964051874,10.2836325373699,12.3016943577019));
#6261=CARTESIAN_POINT('Ctrl Pts',(0.338893825421814,8.86151890835145,13.8465215675306));
#6262=CARTESIAN_POINT('Ctrl Pts',(0.865209614895495,6.87555081718605,14.5283052743907));
#6263=CARTESIAN_POINT('Ctrl Pts',(1.39152540436918,4.80445083237721,14.1826998129294));
#6264=CARTESIAN_POINT('Ctrl Pts',(1.91784119384286,3.14746277801558,12.8930142428118));
#6265=CARTESIAN_POINT('Ctrl Pts',(2.44415698331655,2.30400776307679,10.9701304918164));
#6266=CARTESIAN_POINT('Ctrl Pts',(2.97047277279023,2.47740272551435,8.87756449069058));
#6267=CARTESIAN_POINT('Ctrl Pts',(3.49678856226392,3.62585037656322,7.11973450037077));
#6268=CARTESIAN_POINT('Ctrl Pts',(4.0231043517376,5.47251454159105,6.12036983035809));
#6269=CARTESIAN_POINT('Ctrl Pts',(4.54942014121128,7.57225221141157,6.12036983035694));
#6270=CARTESIAN_POINT('Ctrl Pts',(5.07573593068497,9.41891637644078,7.11973450037252));
#6271=CARTESIAN_POINT('Ctrl Pts',(5.60205172015865,10.5673640274861,8.87756449068726));
#6272=CARTESIAN_POINT('Ctrl Pts',(6.12836750963234,10.7407589899312,10.9701304918231));
#6273=CARTESIAN_POINT('Ctrl Pts',(6.65468329910602,9.89730397497684,12.8930142427982));
#6274=CARTESIAN_POINT('Ctrl Pts',(7.18099908857971,8.24031592064724,14.1826998129572));
#6275=CARTESIAN_POINT('Ctrl Pts',(7.70731487805339,6.16921593577277,14.5283052743338));
#6276=CARTESIAN_POINT('Ctrl Pts',(8.23363066752707,4.18324784474184,13.8465215676471));
#6277=CARTESIAN_POINT('Ctrl Pts',(8.75994645700076,2.76113421544798,12.3016943574634));
#6278=CARTESIAN_POINT('Ctrl Pts',(9.28626224647444,2.24567909126825,10.2662081026629));
#6279=CARTESIAN_POINT('Ctrl Pts',(9.81257803594813,2.76113421485637,8.23072184564557));
#6280=CARTESIAN_POINT('Ctrl Pts',(10.3388938254218,4.18324784624253,6.68589463886829));
#6281=CARTESIAN_POINT('Ctrl Pts',(10.8652096148955,6.16921593255766,6.00411092575748));
#6282=CARTESIAN_POINT('Ctrl Pts',(11.3915254043692,8.24031592730209,6.34971640002317));
#6283=CARTESIAN_POINT('Ctrl Pts',(11.9178411938429,9.89730396131102,7.63940194391146));
#6284=CARTESIAN_POINT('Ctrl Pts',(12.4441569833166,10.7407590179416,9.56228574863674));
#6285=CARTESIAN_POINT('Ctrl Pts',(12.9704727727902,10.5673639700999,11.6548516396987));
#6286=CARTESIAN_POINT('Ctrl Pts',(13.4967885622639,9.41891649399846,13.4126818554805));
#6287=CARTESIAN_POINT('Ctrl Pts',(14.0231043517376,7.57225197059683,14.4120460636421));
#6288=CARTESIAN_POINT('Ctrl Pts',(14.5494201412113,5.47251503489256,14.4120470097292));
#6289=CARTESIAN_POINT('Ctrl Pts',(15.075735930685,3.62584936605174,13.4126804016895));
#6290=CARTESIAN_POINT('Ctrl Pts',(15.6020517201587,2.47740479551235,11.6548543813499));
#6291=CARTESIAN_POINT('Ctrl Pts',(16.1283675096323,2.3040035227468,9.56228024785199));
#6292=CARTESIAN_POINT('Ctrl Pts',(16.654683299106,3.14747146421384,7.63941315580675));
#6293=CARTESIAN_POINT('Ctrl Pts',(17.1809990885797,4.8044330356847,6.34969345866343));
#6294=CARTESIAN_POINT('Ctrl Pts',(17.7073148780534,6.87558727517879,6.00415792274244));
#6295=CARTESIAN_POINT('Ctrl Pts',(18.2336306675271,8.86144321099575,6.68579789056262));
#6296=CARTESIAN_POINT('Ctrl Pts',(18.7599464570008,10.2837860836795,8.2309238623796));
#6297=CARTESIAN_POINT('Ctrl Pts',(19.1108236499832,10.6269009396766,9.58741065714448));
#6298=CARTESIAN_POINT('Ctrl Pts',(19.2862622464744,10.6269009396766,10.2662081021742));
#6299=CARTESIAN_POINT('Ctrl Pts',(-19.7457114929758,10.4071350764215,10.2662081021742));
#6300=CARTESIAN_POINT('Ctrl Pts',(-19.5702728964846,10.4071350764215,10.9084043652423));
#6301=CARTESIAN_POINT('Ctrl Pts',(-19.2193957035022,10.0823325493499,12.1926343284582));
#6302=CARTESIAN_POINT('Ctrl Pts',(-18.6930799140285,8.73618816242606,13.6548102650382));
#6303=CARTESIAN_POINT('Ctrl Pts',(-18.1667641245548,6.85666770773358,14.3000436650509));
#6304=CARTESIAN_POINT('Ctrl Pts',(-17.6404483350811,4.89643689599662,13.9729653727187));
#6305=CARTESIAN_POINT('Ctrl Pts',(-17.1141325456074,3.32820773301878,12.7523373600644));
#6306=CARTESIAN_POINT('Ctrl Pts',(-16.5878167561337,2.52991174299703,10.9324346770084));
#6307=CARTESIAN_POINT('Ctrl Pts',(-16.06150096666,2.6940260673621,8.95193006946043));
#6308=CARTESIAN_POINT('Ctrl Pts',(-15.5351851771864,3.78096813308012,7.28823856150342));
#6309=CARTESIAN_POINT('Ctrl Pts',(-15.0088693877127,5.52873877803479,6.34239253706168));
#6310=CARTESIAN_POINT('Ctrl Pts',(-14.482553598239,7.5160281836638,6.34239279277549));
#6311=CARTESIAN_POINT('Ctrl Pts',(-13.9562378087653,9.26379788184228,7.2882381685645));
#6312=CARTESIAN_POINT('Ctrl Pts',(-13.4299220192916,10.3507423491866,8.95193081048946));
#6313=CARTESIAN_POINT('Ctrl Pts',(-12.9036062298179,10.514851528268,10.9324331902276));
#6314=CARTESIAN_POINT('Ctrl Pts',(-12.3772904403443,9.71656618835865,12.7523403904543));
#6315=CARTESIAN_POINT('Ctrl Pts',(-11.8509746508706,8.14831515246027,13.9729591727957));
#6316=CARTESIAN_POINT('Ctrl Pts',(-11.3246588613969,6.18812917735599,14.3000563616202));
#6317=CARTESIAN_POINT('Ctrl Pts',(-10.7983430719232,4.30851602335673,13.6547843477414));
#6318=CARTESIAN_POINT('Ctrl Pts',(-10.2720272824495,2.96256111851024,12.1926875689854));
#6319=CARTESIAN_POINT('Ctrl Pts',(-9.74571149297584,2.47471026267615,10.2662081020422));
#6320=CARTESIAN_POINT('Ctrl Pts',(-9.21939570350214,2.96256111899924,8.33972863569814));
#6321=CARTESIAN_POINT('Ctrl Pts',(-8.69307991402848,4.30851602211631,6.87763185602132));
#6322=CARTESIAN_POINT('Ctrl Pts',(-8.16676412455478,6.18812918001347,6.23235984387893));
#6323=CARTESIAN_POINT('Ctrl Pts',(-7.64044833508111,8.14831514695963,6.55945702921968));
#6324=CARTESIAN_POINT('Ctrl Pts',(-7.11413254560742,9.7165661996543,7.78007581866172));
#6325=CARTESIAN_POINT('Ctrl Pts',(-6.58781675613373,10.5148515051157,9.59998300436044));
#6326=CARTESIAN_POINT('Ctrl Pts',(-6.06150096666004,10.3507423966199,11.58048541385));
#6327=CARTESIAN_POINT('Ctrl Pts',(-5.53518517718637,9.26379778467361,13.2441779948344));
#6328=CARTESIAN_POINT('Ctrl Pts',(-5.00886938771268,7.51602838271203,14.190023495456));
#6329=CARTESIAN_POINT('Ctrl Pts',(-4.482553598239,5.52873837029065,14.1900234954557));
#6330=CARTESIAN_POINT('Ctrl Pts',(-3.95623780876531,3.78096896833021,13.2441779948349));
#6331=CARTESIAN_POINT('Ctrl Pts',(-3.42992201929163,2.69402435638103,11.5804854138491));
#6332=CARTESIAN_POINT('Ctrl Pts',(-2.90360622981794,2.52991524789141,9.59998300436223));
#6333=CARTESIAN_POINT('Ctrl Pts',(-2.37729044034426,3.32820055333996,7.78007581865805));
#6334=CARTESIAN_POINT('Ctrl Pts',(-1.85097465087057,4.8964516060611,6.55945702922718));
#6335=CARTESIAN_POINT('Ctrl Pts',(-1.32465886139689,6.856637572953,6.23235984386357));
#6336=CARTESIAN_POINT('Ctrl Pts',(-0.798343071923207,8.7362507309613,6.8776318560528));
#6337=CARTESIAN_POINT('Ctrl Pts',(-0.272027282449524,10.0822056338507,8.33972863563365));
#6338=CARTESIAN_POINT('Ctrl Pts',(0.254288507024159,10.5700564906402,10.2662081021742));
#6339=CARTESIAN_POINT('Ctrl Pts',(0.780604296497844,10.0822056338507,12.1926875687148));
#6340=CARTESIAN_POINT('Ctrl Pts',(1.30692008597153,8.73625073096131,13.6547843482957));
#6341=CARTESIAN_POINT('Ctrl Pts',(1.83323587544521,6.85663757295299,14.3000563604849));
#6342=CARTESIAN_POINT('Ctrl Pts',(2.3595516649189,4.8964516060611,13.9729591751213));
#6343=CARTESIAN_POINT('Ctrl Pts',(2.88586745439258,3.32820055333996,12.7523403856904));
#6344=CARTESIAN_POINT('Ctrl Pts',(3.41218324386627,2.52991524789141,10.9324331999862));
#6345=CARTESIAN_POINT('Ctrl Pts',(3.93849903333995,2.69402435638102,8.95193079049936));
#6346=CARTESIAN_POINT('Ctrl Pts',(4.46481482281363,3.78096896833022,7.28823820951355));
#6347=CARTESIAN_POINT('Ctrl Pts',(4.99113061228732,5.52873837029065,6.34239270889278));
#6348=CARTESIAN_POINT('Ctrl Pts',(5.517446401761,7.51602838271202,6.34239270889247));
#6349=CARTESIAN_POINT('Ctrl Pts',(6.04376219123469,9.2637977846736,7.28823820951402));
#6350=CARTESIAN_POINT('Ctrl Pts',(6.57007798070837,10.3507423966199,8.95193079049845));
#6351=CARTESIAN_POINT('Ctrl Pts',(7.09639377018205,10.5148515051157,10.932433199988));
#6352=CARTESIAN_POINT('Ctrl Pts',(7.62270955965573,9.7165661996543,12.7523403856867));
#6353=CARTESIAN_POINT('Ctrl Pts',(8.14902534912942,8.14831514695962,13.9729591751288));
#6354=CARTESIAN_POINT('Ctrl Pts',(8.67534113860311,6.18812918001348,14.3000563604695));
#6355=CARTESIAN_POINT('Ctrl Pts',(9.20165692807679,4.30851602211632,13.6547843483271));
#6356=CARTESIAN_POINT('Ctrl Pts',(9.72797271755048,2.96256111899924,12.1926875686503));
#6357=CARTESIAN_POINT('Ctrl Pts',(10.2542885070242,2.47471026267615,10.2662081023063));
#6358=CARTESIAN_POINT('Ctrl Pts',(10.7806042964978,2.96256111851024,8.33972863536311));
#6359=CARTESIAN_POINT('Ctrl Pts',(11.3069200859715,4.30851602335673,6.877631856607));
#6360=CARTESIAN_POINT('Ctrl Pts',(11.8332358754452,6.18812917735599,6.23235984272829));
#6361=CARTESIAN_POINT('Ctrl Pts',(12.3595516649189,8.14831515246027,6.55945703155276));
#6362=CARTESIAN_POINT('Ctrl Pts',(12.8858674543926,9.71656618835865,7.7800758138942));
#6363=CARTESIAN_POINT('Ctrl Pts',(13.4121832438663,10.514851528268,9.59998301412081));
#6364=CARTESIAN_POINT('Ctrl Pts',(13.9384990333399,10.3507423491866,11.580485393859));
#6365=CARTESIAN_POINT('Ctrl Pts',(14.4648148228136,9.26379788184228,13.244178035784));
#6366=CARTESIAN_POINT('Ctrl Pts',(14.9911306122873,7.51602818366379,14.190023411573));
#6367=CARTESIAN_POINT('Ctrl Pts',(15.517446401761,5.52873877803478,14.1900236672868));
#6368=CARTESIAN_POINT('Ctrl Pts',(16.0437621912347,3.78096813308012,13.244177642845));
#6369=CARTESIAN_POINT('Ctrl Pts',(16.5700779807084,2.6940260673621,11.580486134888));
#6370=CARTESIAN_POINT('Ctrl Pts',(17.0963937701821,2.52991174299704,9.59998152734011));
#6371=CARTESIAN_POINT('Ctrl Pts',(17.6227095596557,3.32820773301878,7.78007884428401));
#6372=CARTESIAN_POINT('Ctrl Pts',(18.1490253491294,4.89643689599663,6.55945083162973));
#6373=CARTESIAN_POINT('Ctrl Pts',(18.6753411386031,6.85666770773357,6.23237253929761));
#6374=CARTESIAN_POINT('Ctrl Pts',(19.2016569280768,8.73618816242606,6.87760593931028));
#6375=CARTESIAN_POINT('Ctrl Pts',(19.7279727175505,10.0823325493499,8.3397818758903));
#6376=CARTESIAN_POINT('Ctrl Pts',(20.0788499105329,10.4071350764215,9.62401183910617));
#6377=CARTESIAN_POINT('Ctrl Pts',(20.2542885070242,10.4071350764215,10.2662081021742));
#6378=CARTESIAN_POINT('Ctrl Pts',(-18.9673979627111,11.0253866956159,10.2662081021742));
#6379=CARTESIAN_POINT('Ctrl Pts',(-18.7919593662199,11.0253866956159,11.0108242444962));
#6380=CARTESIAN_POINT('Ctrl Pts',(-18.4410821732374,10.648941808576,12.499124383921));
#6381=CARTESIAN_POINT('Ctrl Pts',(-17.9147663837637,9.08852492824315,14.1941879499634));
#6382=CARTESIAN_POINT('Ctrl Pts',(-17.3884505942901,6.90987534694561,14.9420335378486));
#6383=CARTESIAN_POINT('Ctrl Pts',(-16.8621348048164,4.63765298021549,14.5629378567814));
#6384=CARTESIAN_POINT('Ctrl Pts',(-16.3358190153427,2.8198305198544,13.1480179635823));
#6385=CARTESIAN_POINT('Ctrl Pts',(-15.809503225869,1.89447816606942,11.0384729586759));
#6386=CARTESIAN_POINT('Ctrl Pts',(-15.2831874363953,2.08471320623785,8.74275090650475));
#6387=CARTESIAN_POINT('Ctrl Pts',(-14.7568716469216,3.3446503103771,6.81427210911637));
#6388=CARTESIAN_POINT('Ctrl Pts',(-14.2305558574479,5.3705925024193,5.71788617736171));
#6389=CARTESIAN_POINT('Ctrl Pts',(-13.7042400679743,7.67417451789751,5.71788701062985));
#6390=CARTESIAN_POINT('Ctrl Pts',(-13.1779242785006,9.70011549723399,6.81427082868689));
#6391=CARTESIAN_POINT('Ctrl Pts',(-12.6516084890269,10.9600556775659,8.74275332121974));
#6392=CARTESIAN_POINT('Ctrl Pts',(-12.1252926995532,11.1502841272486,11.0384681138492));
#6393=CARTESIAN_POINT('Ctrl Pts',(-11.5989769100795,10.2249454149688,13.1480278384744));
#6394=CARTESIAN_POINT('Ctrl Pts',(-11.0726611206058,8.40709493804338,14.5629176513865));
#6395=CARTESIAN_POINT('Ctrl Pts',(-10.5463453311322,6.13493000161398,14.9420749286073));
#6396=CARTESIAN_POINT('Ctrl Pts',(-10.0200295416585,3.95616168372213,14.194102813041));
#6397=CARTESIAN_POINT('Ctrl Pts',(-9.49371375218478,2.39598750700088,12.499301874919));
#6398=CARTESIAN_POINT('Ctrl Pts',(-8.96739796271111,1.83049136418784,10.2662081017439));
#6399=CARTESIAN_POINT('Ctrl Pts',(-8.44108217323742,2.39598750762722,8.03311433052112));
#6400=CARTESIAN_POINT('Ctrl Pts',(-7.91476638376373,3.95616168213331,6.33831338939892));
#6401=CARTESIAN_POINT('Ctrl Pts',(-7.38845059429005,6.13493000501789,5.59034127949062));
#6402=CARTESIAN_POINT('Ctrl Pts',(-6.86213480481637,8.40709493099772,5.96949854535944));
#6403=CARTESIAN_POINT('Ctrl Pts',(-6.33581901534268,10.2249454294372,7.38438838140947));
#6404=CARTESIAN_POINT('Ctrl Pts',(-5.809503225869,11.1502840975933,9.49394805869413));
#6405=CARTESIAN_POINT('Ctrl Pts',(-5.28318743639531,10.9600557383222,11.7896629482713));
#6406=CARTESIAN_POINT('Ctrl Pts',(-4.75687164692163,9.70011537277267,13.7181452422236));
#6407=CARTESIAN_POINT('Ctrl Pts',(-4.23055585744794,7.67417477285422,14.8145294670595));
#6408=CARTESIAN_POINT('Ctrl Pts',(-3.70424006797426,5.37059198014839,14.8145294670585));
#6409=CARTESIAN_POINT('Ctrl Pts',(-3.17792427850058,3.3446513802314,13.7181452422251));
#6410=CARTESIAN_POINT('Ctrl Pts',(-2.65160848902689,2.08471101467814,11.7896629482684));
#6411=CARTESIAN_POINT('Ctrl Pts',(-2.12529269955321,1.89448265541499,9.49394805869999));
#6412=CARTESIAN_POINT('Ctrl Pts',(-1.59897691007952,2.81982132355466,7.38438838139752));
#6413=CARTESIAN_POINT('Ctrl Pts',(-1.07266112060584,4.63767182202801,5.96949854538387));
#6414=CARTESIAN_POINT('Ctrl Pts',(-0.546345331132152,6.90983674793835,5.59034127944055));
#6415=CARTESIAN_POINT('Ctrl Pts',(-0.0200295416584694,9.08860507096528,
6.33831338950149));
#6416=CARTESIAN_POINT('Ctrl Pts',(0.506286247815215,10.6487792451797,8.03311433031102));
#6417=CARTESIAN_POINT('Ctrl Pts',(1.0326020372889,11.2142753892165,10.2662081021742));
#6418=CARTESIAN_POINT('Ctrl Pts',(1.55891782676258,10.6487792451797,12.4993018740374));
#6419=CARTESIAN_POINT('Ctrl Pts',(2.08523361623627,9.0886050709653,14.194102814847));
#6420=CARTESIAN_POINT('Ctrl Pts',(2.61154940570995,6.90983674793834,14.9420749249079));
#6421=CARTESIAN_POINT('Ctrl Pts',(3.13786519518364,4.63767182202801,14.5629176589646));
#6422=CARTESIAN_POINT('Ctrl Pts',(3.66418098465732,2.81982132355465,13.1480278229509));
#6423=CARTESIAN_POINT('Ctrl Pts',(4.19049677413101,1.89448265541498,11.0384681456485));
#6424=CARTESIAN_POINT('Ctrl Pts',(4.71681256360468,2.08471101467815,8.74275325608004));
#6425=CARTESIAN_POINT('Ctrl Pts',(5.24312835307838,3.3446513802314,6.81427096212333));
#6426=CARTESIAN_POINT('Ctrl Pts',(5.76944414255205,5.3705919801484,5.71788673728997));
#6427=CARTESIAN_POINT('Ctrl Pts',(6.29575993202575,7.67417477285421,5.71788673728895));
#6428=CARTESIAN_POINT('Ctrl Pts',(6.82207572149942,9.70011537277266,6.81427096212487));
#6429=CARTESIAN_POINT('Ctrl Pts',(7.34839151097311,10.9600557383222,8.7427532560771));
#6430=CARTESIAN_POINT('Ctrl Pts',(7.8747073004468,11.1502840975933,11.0384681456543));
#6431=CARTESIAN_POINT('Ctrl Pts',(8.40102308992048,10.2249454294372,13.148027822939));
#6432=CARTESIAN_POINT('Ctrl Pts',(8.92733887939416,8.40709493099771,14.562917658989));
#6433=CARTESIAN_POINT('Ctrl Pts',(9.45365466886784,6.13493000501789,14.9420749248578));
#6434=CARTESIAN_POINT('Ctrl Pts',(9.97997045834153,3.9561616821333,14.1941028149495));
#6435=CARTESIAN_POINT('Ctrl Pts',(10.5062862478152,2.39598750762723,12.4993018738273));
#6436=CARTESIAN_POINT('Ctrl Pts',(11.0326020372889,1.83049136418784,10.2662081026046));
#6437=CARTESIAN_POINT('Ctrl Pts',(11.5589178267626,2.39598750700087,8.03311432942944));
#6438=CARTESIAN_POINT('Ctrl Pts',(12.0852336162363,3.95616168372213,6.33831339130741));
#6439=CARTESIAN_POINT('Ctrl Pts',(12.61154940571,6.13493000161398,5.59034127574115));
#6440=CARTESIAN_POINT('Ctrl Pts',(13.1378651951836,8.40709493804338,5.96949855296197));
#6441=CARTESIAN_POINT('Ctrl Pts',(13.6641809846573,10.2249454149688,7.38438836587406));
#6442=CARTESIAN_POINT('Ctrl Pts',(14.190496774131,11.1502841272486,9.49394809049926));
#6443=CARTESIAN_POINT('Ctrl Pts',(14.7168125636047,10.9600556775659,11.7896628831287));
#6444=CARTESIAN_POINT('Ctrl Pts',(15.2431283530784,9.70011549723399,13.7181453756616));
#6445=CARTESIAN_POINT('Ctrl Pts',(15.7694441425521,7.67417451789751,14.8145291937186));
#6446=CARTESIAN_POINT('Ctrl Pts',(16.2957599320257,5.37059250241929,14.8145300269868));
#6447=CARTESIAN_POINT('Ctrl Pts',(16.8220757214994,3.3446503103771,13.7181440952321));
#6448=CARTESIAN_POINT('Ctrl Pts',(17.3483915109731,2.08471320623786,11.7896652978437));
#6449=CARTESIAN_POINT('Ctrl Pts',(17.8747073004468,1.89447816606942,9.49394324567252));
#6450=CARTESIAN_POINT('Ctrl Pts',(18.4010230899205,2.8198305198544,7.38439824076613));
#6451=CARTESIAN_POINT('Ctrl Pts',(18.9273388793942,4.63765298021549,5.96947834756709));
#6452=CARTESIAN_POINT('Ctrl Pts',(19.4536546688679,6.90987534694561,5.59038266649988));
#6453=CARTESIAN_POINT('Ctrl Pts',(19.9799704583415,9.08852492824313,6.33822825438502));
#6454=CARTESIAN_POINT('Ctrl Pts',(20.5062862478152,10.648941808576,8.03329182042749));
#6455=CARTESIAN_POINT('Ctrl Pts',(20.8571634407977,11.0253866956159,9.52159195985228));
#6456=CARTESIAN_POINT('Ctrl Pts',(21.0326020372889,11.0253866956159,10.2662081021742));
#6457=CARTESIAN_POINT('Ctrl Pts',(-18.9696903481015,12.0184298315526,10.2662081021742));
#6458=CARTESIAN_POINT('Ctrl Pts',(-18.7942517516103,12.0184298315526,11.1750396528639));
#6459=CARTESIAN_POINT('Ctrl Pts',(-18.4433745586278,11.5589692572687,12.9915446672008));
#6460=CARTESIAN_POINT('Ctrl Pts',(-17.9170587691541,9.65443410911255,15.0604240895053));
#6461=CARTESIAN_POINT('Ctrl Pts',(-17.3907429796805,6.99532877884549,15.9731892980894));
#6462=CARTESIAN_POINT('Ctrl Pts',(-16.8644271902068,4.22201466394135,15.5104930007101));
#6463=CARTESIAN_POINT('Ctrl Pts',(-16.3381114007331,2.00330916936381,13.7835412891382));
#6464=CARTESIAN_POINT('Ctrl Pts',(-15.8117956112594,0.873889476925023,11.2087800686737));
#6465=CARTESIAN_POINT('Ctrl Pts',(-15.2854798217857,1.1060769339483,8.40678392236536));
#6466=CARTESIAN_POINT('Ctrl Pts',(-14.759164032312,2.64386707202477,6.05301911539166));
#6467=CARTESIAN_POINT('Ctrl Pts',(-14.2328482428383,5.11658887331684,4.71484793596357));
#6468=CARTESIAN_POINT('Ctrl Pts',(-13.7065324533647,7.92817820664652,4.71484896770077));
#6469=CARTESIAN_POINT('Ctrl Pts',(-13.180216663891,10.4008985246382,6.05301752998757));
#6470=CARTESIAN_POINT('Ctrl Pts',(-12.6539008744173,11.9386924253073,8.4067869122208));
#6471=CARTESIAN_POINT('Ctrl Pts',(-12.1275850849436,12.1708718212904,11.2087740698988));
#6472=CARTESIAN_POINT('Ctrl Pts',(-11.6012692954699,11.0414688142261,13.7835535160476));
#6473=CARTESIAN_POINT('Ctrl Pts',(-11.0749535059962,8.82272905166539,15.5104679827411));
#6474=CARTESIAN_POINT('Ctrl Pts',(-10.5486377165226,6.04948518165475,15.9732405475343));
#6475=CARTESIAN_POINT('Ctrl Pts',(-10.0223219270489,3.39023462074606,15.0603186678871));
#6476=CARTESIAN_POINT('Ctrl Pts',(-9.49600613757519,1.48599633137589,12.9917644722719));
#6477=CARTESIAN_POINT('Ctrl Pts',(-8.96969034810151,0.795791722368668,10.2662081016414));
#6478=CARTESIAN_POINT('Ctrl Pts',(-8.44337455862781,1.485996332142,7.54065173342831));
#6479=CARTESIAN_POINT('Ctrl Pts',(-7.91705876915414,3.39023461880273,5.47209753409825));
#6480=CARTESIAN_POINT('Ctrl Pts',(-7.39074297968046,6.04948518581819,4.55917566145673));
#6481=CARTESIAN_POINT('Ctrl Pts',(-6.86442719020676,8.82272904304761,5.02194821219404));
#6482=CARTESIAN_POINT('Ctrl Pts',(-6.33811140073309,11.0414688319228,6.7488627075365));
#6483=CARTESIAN_POINT('Ctrl Pts',(-5.8117956112594,12.170871785018,9.32364209506915));
#6484=CARTESIAN_POINT('Ctrl Pts',(-5.28547982178571,11.9386924996204,12.1256293727861));
#6485=CARTESIAN_POINT('Ctrl Pts',(-4.75916403231203,10.4008983724055,14.4793985091405));
#6486=CARTESIAN_POINT('Ctrl Pts',(-4.23284824283835,7.92817851849246,15.8175675750933));
#6487=CARTESIAN_POINT('Ctrl Pts',(-3.70653245336467,5.11658823451009,15.8175675750921));
#6488=CARTESIAN_POINT('Ctrl Pts',(-3.18021666389098,2.64386838059882,14.4793985091424));
#6489=CARTESIAN_POINT('Ctrl Pts',(-2.6539008744173,1.1060742533794,12.1256293727824));
#6490=CARTESIAN_POINT('Ctrl Pts',(-2.12758508494361,0.873894967991537,9.3236420950764));
#6491=CARTESIAN_POINT('Ctrl Pts',(-1.60126929546993,2.00329792106653,6.74886270752171));
#6492=CARTESIAN_POINT('Ctrl Pts',(-1.07495350599624,4.2220377099832,5.02194821222431));
#6493=CARTESIAN_POINT('Ctrl Pts',(-0.548637716522558,6.99528156712763,4.55917566139474));
#6494=CARTESIAN_POINT('Ctrl Pts',(-0.0223219270488751,9.65453213431721,
5.47209753422524));
#6495=CARTESIAN_POINT('Ctrl Pts',(0.503993862424809,11.5587704206212,7.54065173316817));
#6496=CARTESIAN_POINT('Ctrl Pts',(1.03030965189849,12.2489750311253,10.2662081021742));
#6497=CARTESIAN_POINT('Ctrl Pts',(1.55662544137218,11.5587704206212,12.9917644711803));
#6498=CARTESIAN_POINT('Ctrl Pts',(2.08294123084587,9.65453213431721,15.0603186701232));
#6499=CARTESIAN_POINT('Ctrl Pts',(2.60925702031954,6.99528156712763,15.9732405429537));
#6500=CARTESIAN_POINT('Ctrl Pts',(3.13557280979324,4.22203770998318,15.5104679921241));
#6501=CARTESIAN_POINT('Ctrl Pts',(3.66188859926691,2.00329792106652,13.7835534968268));
#6502=CARTESIAN_POINT('Ctrl Pts',(4.18820438874061,0.873894967991535,11.2087741092721));
#6503=CARTESIAN_POINT('Ctrl Pts',(4.71452017821428,1.1060742533794,8.40678683156602));
#6504=CARTESIAN_POINT('Ctrl Pts',(5.24083596768797,2.64386838059882,6.05301769520609));
#6505=CARTESIAN_POINT('Ctrl Pts',(5.76715175716164,5.11658823451008,4.71484862925638));
#6506=CARTESIAN_POINT('Ctrl Pts',(6.29346754663534,7.92817851849245,4.71484862925513));
#6507=CARTESIAN_POINT('Ctrl Pts',(6.81978333610902,10.4008983724055,6.053017695208));
#6508=CARTESIAN_POINT('Ctrl Pts',(7.3460991255827,11.9386924996204,8.40678683156239));
#6509=CARTESIAN_POINT('Ctrl Pts',(7.87241491505639,12.170871785018,11.2087741092793));
#6510=CARTESIAN_POINT('Ctrl Pts',(8.39873070453007,11.0414688319228,13.783553496812));
#6511=CARTESIAN_POINT('Ctrl Pts',(8.92504649400376,8.82272904304761,15.5104679921544));
#6512=CARTESIAN_POINT('Ctrl Pts',(9.45136228347744,6.04948518581819,15.9732405428917));
#6513=CARTESIAN_POINT('Ctrl Pts',(9.97767807295112,3.39023461880273,15.0603186702502));
#6514=CARTESIAN_POINT('Ctrl Pts',(10.5039938624248,1.48599633214201,12.9917644709202));
#6515=CARTESIAN_POINT('Ctrl Pts',(11.0303096518985,0.795791722368667,10.2662081027071));
#6516=CARTESIAN_POINT('Ctrl Pts',(11.5566254413722,1.48599633137589,7.54065173207658));
#6517=CARTESIAN_POINT('Ctrl Pts',(12.0829412308458,3.39023462074607,5.47209753646132));
#6518=CARTESIAN_POINT('Ctrl Pts',(12.6092570203196,6.04948518165476,4.5591756568142));
#6519=CARTESIAN_POINT('Ctrl Pts',(13.1355728097932,8.82272905166539,5.02194822160738));
#6520=CARTESIAN_POINT('Ctrl Pts',(13.6618885992669,11.0414688142261,6.74886268830085));
#6521=CARTESIAN_POINT('Ctrl Pts',(14.1882043887406,12.1708718212903,9.32364213444966));
#6522=CARTESIAN_POINT('Ctrl Pts',(14.7145201782143,11.9386924253074,12.1256292921277));
#6523=CARTESIAN_POINT('Ctrl Pts',(15.240835967688,10.4008985246382,14.4793986743609));
#6524=CARTESIAN_POINT('Ctrl Pts',(15.7671517571617,7.9281782066465,15.8175672366477));
#6525=CARTESIAN_POINT('Ctrl Pts',(16.2934675466353,5.11658887331682,15.8175682683849));
#6526=CARTESIAN_POINT('Ctrl Pts',(16.819783336109,2.64386707202477,14.4793970889568));
#6527=CARTESIAN_POINT('Ctrl Pts',(17.3460991255827,1.10607693394831,12.1256322819831));
#6528=CARTESIAN_POINT('Ctrl Pts',(17.8724149150564,0.87388947692502,9.32363613567474));
#6529=CARTESIAN_POINT('Ctrl Pts',(18.3987307045301,2.00330916936382,6.74887491521026));
#6530=CARTESIAN_POINT('Ctrl Pts',(18.9250464940037,4.22201466394136,5.02192320363833));
#6531=CARTESIAN_POINT('Ctrl Pts',(19.4513622834774,6.99532877884548,4.5592269062591));
#6532=CARTESIAN_POINT('Ctrl Pts',(19.9776780729511,9.65443410911256,5.47199211484313));
#6533=CARTESIAN_POINT('Ctrl Pts',(20.5039938624248,11.5589692572687,7.54087153714766));
#6534=CARTESIAN_POINT('Ctrl Pts',(20.8548710554073,12.0184298315526,9.35737655148451));
#6535=CARTESIAN_POINT('Ctrl Pts',(21.0303096518985,12.0184298315526,10.2662081021742));
#6536=CARTESIAN_POINT('Ctrl Pts',(-19.7447240968701,12.6400132078441,10.2662081021742));
#6537=CARTESIAN_POINT('Ctrl Pts',(-19.5692855003789,12.6400132078441,11.2775286623238));
#6538=CARTESIAN_POINT('Ctrl Pts',(-19.2184083073964,12.1285212433829,13.2999046745019));
#6539=CARTESIAN_POINT('Ctrl Pts',(-18.6920925179228,10.0086393556897,15.602512565909));
#6540=CARTESIAN_POINT('Ctrl Pts',(-18.1657767284491,7.04880778687935,16.6186123849351));
#6541=CARTESIAN_POINT('Ctrl Pts',(-17.6394609389754,3.96187493613662,16.103536433244));
#6542=CARTESIAN_POINT('Ctrl Pts',(-17.1131451495017,1.4922586425256,14.1813152991222));
#6543=CARTESIAN_POINT('Ctrl Pts',(-16.586829360028,0.235117861288675,11.3153685977046));
#6544=CARTESIAN_POINT('Ctrl Pts',(-16.0605135705543,0.493561867166209,8.19650898389307));
#6545=CARTESIAN_POINT('Ctrl Pts',(-15.5341977810806,2.20525677030406,5.57656046896309));
#6546=CARTESIAN_POINT('Ctrl Pts',(-15.007881991607,4.95761147974642,4.08706080887933));
#6547=CARTESIAN_POINT('Ctrl Pts',(-14.4815662021333,8.08715560221738,4.08706121814656));
#6548=CARTESIAN_POINT('Ctrl Pts',(-13.9552504126596,10.8395088192841,5.57655984006851));
#6549=CARTESIAN_POINT('Ctrl Pts',(-13.4289346231859,12.5512075080354,8.19651016990216));
#6550=CARTESIAN_POINT('Ctrl Pts',(-12.9026188337123,12.8096434035524,11.3153662181278));
#6551=CARTESIAN_POINT('Ctrl Pts',(-12.3763030442385,11.5525194097769,14.1813201492298));
#6552=CARTESIAN_POINT('Ctrl Pts',(-11.8499872547649,9.08286863851945,16.1035265103043));
#6553=CARTESIAN_POINT('Ctrl Pts',(-11.3236714652912,5.99600646245248,16.6186327058768));
#6554=CARTESIAN_POINT('Ctrl Pts',(-10.7973556758175,3.03602877442981,15.6024710771885));
#6555=CARTESIAN_POINT('Ctrl Pts',(-10.2710398863438,0.91644556180598,13.299989934402));
#6556=CARTESIAN_POINT('Ctrl Pts',(-9.74472409687013,0.148187665078963,10.2662081019628));
#6557=CARTESIAN_POINT('Ctrl Pts',(-9.21840830739645,0.91644556257677,7.23242627048267));
#6558=CARTESIAN_POINT('Ctrl Pts',(-8.69209251792277,3.03602877247459,4.92994512622261));
#6559=CARTESIAN_POINT('Ctrl Pts',(-8.16577672844908,5.99600646664137,3.91378350031322));
#6560=CARTESIAN_POINT('Ctrl Pts',(-7.6394609389754,9.08286862984897,4.42888969031004));
#6561=CARTESIAN_POINT('Ctrl Pts',(-7.11314514950171,11.5525194275819,6.35109606274901));
#6562=CARTESIAN_POINT('Ctrl Pts',(-6.58682936002803,12.8096433670582,9.21704997059926));
#6563=CARTESIAN_POINT('Ctrl Pts',(-6.06051357055434,12.5512075828031,12.3359060664417));
#6564=CARTESIAN_POINT('Ctrl Pts',(-5.53419778108066,10.8395086661199,14.9558562987407));
#6565=CARTESIAN_POINT('Ctrl Pts',(-5.00788199160698,8.08715591597131,16.4453551204558));
#6566=CARTESIAN_POINT('Ctrl Pts',(-4.48156620213329,4.95761083703122,16.4453551204553));
#6567=CARTESIAN_POINT('Ctrl Pts',(-3.95525041265961,2.20525808688441,14.9558562987414));
#6568=CARTESIAN_POINT('Ctrl Pts',(-3.42893462318592,0.493559170196666,12.3359060664403));
#6569=CARTESIAN_POINT('Ctrl Pts',(-2.90261883371224,0.235123385951408,9.21704997060214));
#6570=CARTESIAN_POINT('Ctrl Pts',(-2.37630304423856,1.49224732540739,6.35109606274313));
#6571=CARTESIAN_POINT('Ctrl Pts',(-1.84998725476487,3.96189812318202,4.42888969032205));
#6572=CARTESIAN_POINT('Ctrl Pts',(-1.32367146529119,7.04876028630408,3.91378350028863));
#6573=CARTESIAN_POINT('Ctrl Pts',(-0.797355675817504,10.0087379806461,4.92994512627298));
#6574=CARTESIAN_POINT('Ctrl Pts',(-0.27103988634382,12.128321190185,7.23242627037947));
#6575=CARTESIAN_POINT('Ctrl Pts',(0.255275903129863,12.896579088418,10.2662081021742));
#6576=CARTESIAN_POINT('Ctrl Pts',(0.781591692603546,12.128321190185,13.299989933969));
#6577=CARTESIAN_POINT('Ctrl Pts',(1.30790748207723,10.0087379806461,15.6024710780755));
#6578=CARTESIAN_POINT('Ctrl Pts',(1.83422327155091,7.04876028630408,16.6186327040598));
#6579=CARTESIAN_POINT('Ctrl Pts',(2.3605390610246,3.96189812318201,16.1035265140264));
#6580=CARTESIAN_POINT('Ctrl Pts',(2.88685485049829,1.49224732540738,14.1813201416053));
#6581=CARTESIAN_POINT('Ctrl Pts',(3.41317063997197,0.235123385951407,11.3153662337463));
#6582=CARTESIAN_POINT('Ctrl Pts',(3.93948642944565,0.49355917019667,8.1965101379082));
#6583=CARTESIAN_POINT('Ctrl Pts',(4.46580221891934,2.2052580868844,5.57655990560704));
#6584=CARTESIAN_POINT('Ctrl Pts',(4.99211800839302,4.95761083703123,4.08706108389318));
#6585=CARTESIAN_POINT('Ctrl Pts',(5.5184337978667,8.08715591597129,4.08706108389269));
#6586=CARTESIAN_POINT('Ctrl Pts',(6.04474958734038,10.8395086661199,5.57655990560779));
#6587=CARTESIAN_POINT('Ctrl Pts',(6.57106537681407,12.5512075828031,8.19651013790676));
#6588=CARTESIAN_POINT('Ctrl Pts',(7.09738116628776,12.8096433670582,11.3153662337492));
#6589=CARTESIAN_POINT('Ctrl Pts',(7.62369695576144,11.5525194275819,14.1813201415994));
#6590=CARTESIAN_POINT('Ctrl Pts',(8.15001274523513,9.08286862984896,16.1035265140384));
#6591=CARTESIAN_POINT('Ctrl Pts',(8.67632853470882,5.99600646664138,16.6186327040352));
#6592=CARTESIAN_POINT('Ctrl Pts',(9.20264432418249,3.03602877247459,15.6024710781259));
#6593=CARTESIAN_POINT('Ctrl Pts',(9.72896011365618,0.916445562576777,13.2999899338658));
#6594=CARTESIAN_POINT('Ctrl Pts',(10.2552759031299,0.148187665078963,10.2662081023856));
#6595=CARTESIAN_POINT('Ctrl Pts',(10.7815916926035,0.916445561805976,7.23242626994647));
#6596=CARTESIAN_POINT('Ctrl Pts',(11.3079074820772,3.03602877442982,4.92994512715997));
#6597=CARTESIAN_POINT('Ctrl Pts',(11.8342232715509,5.99600646245248,3.91378349847164));
#6598=CARTESIAN_POINT('Ctrl Pts',(12.3605390610246,9.08286863851947,4.4288896940441));
#6599=CARTESIAN_POINT('Ctrl Pts',(12.8868548504983,11.5525194097769,6.35109605511865));
#6600=CARTESIAN_POINT('Ctrl Pts',(13.413170639972,12.8096434035524,9.21704998622064));
#6601=CARTESIAN_POINT('Ctrl Pts',(13.9394864294457,12.5512075080354,12.3359060344463));
#6602=CARTESIAN_POINT('Ctrl Pts',(14.4658022189193,10.8395088192841,14.9558563642799));
#6603=CARTESIAN_POINT('Ctrl Pts',(14.992118008393,8.08715560221737,16.4453549862019));
#6604=CARTESIAN_POINT('Ctrl Pts',(15.5184337978667,4.9576114797464,16.4453553954691));
#6605=CARTESIAN_POINT('Ctrl Pts',(16.0447495873404,2.20525677030405,14.9558557353854));
#6606=CARTESIAN_POINT('Ctrl Pts',(16.5710653768141,0.493561867166209,12.3359072204554));
#6607=CARTESIAN_POINT('Ctrl Pts',(17.0973811662878,0.235117861288674,9.21704760664382));
#6608=CARTESIAN_POINT('Ctrl Pts',(17.6236969557614,1.4922586425256,6.35110090522623));
#6609=CARTESIAN_POINT('Ctrl Pts',(18.1500127452351,3.96187493613663,4.42887977110448));
#6610=CARTESIAN_POINT('Ctrl Pts',(18.6763285347088,7.04880778687935,3.91380381941334));
#6611=CARTESIAN_POINT('Ctrl Pts',(19.2026443241825,10.0086393556897,4.92990363843943));
#6612=CARTESIAN_POINT('Ctrl Pts',(19.7289601136562,12.1285212433829,7.23251152984658));
#6613=CARTESIAN_POINT('Ctrl Pts',(20.0798373066386,12.6400132078441,9.25488754202469));
#6614=CARTESIAN_POINT('Ctrl Pts',(20.2552759031298,12.6400132078441,10.2662081021742));
#6615=CARTESIAN_POINT('Ctrl Pts',(-20.7138122396522,12.4160945610234,10.2662081021742));
#6616=CARTESIAN_POINT('Ctrl Pts',(-20.538373643161,12.4160945610234,11.2408846067237));
#6617=CARTESIAN_POINT('Ctrl Pts',(-20.1874964501786,11.9234097510006,13.1886963350883));
#6618=CARTESIAN_POINT('Ctrl Pts',(-19.6611806607048,9.8810581004343,15.4073432872781));
#6619=CARTESIAN_POINT('Ctrl Pts',(-19.1348648712312,7.02955135660707,16.3861208997243));
#6620=CARTESIAN_POINT('Ctrl Pts',(-18.6085490817575,4.05556523698548,15.8899610759315));
#6621=CARTESIAN_POINT('Ctrl Pts',(-18.0822332922838,1.67632104728412,14.0380438270458));
#6622=CARTESIAN_POINT('Ctrl Pts',(-17.5559175028101,0.465178955365346,11.2769833767237));
#6623=CARTESIAN_POINT('Ctrl Pts',(-17.0296017133364,0.714167149390354,8.27224020810767));
#6624=CARTESIAN_POINT('Ctrl Pts',(-16.5032859238627,2.36322766355062,5.74816399917117));
#6625=CARTESIAN_POINT('Ctrl Pts',(-15.976970134389,5.01486925380052,4.31316578561841));
#6626=CARTESIAN_POINT('Ctrl Pts',(-15.4506543449154,8.02989786004729,4.31316710813318));
#6627=CARTESIAN_POINT('Ctrl Pts',(-14.9243385554417,10.6815378132754,5.74816196694792));
#6628=CARTESIAN_POINT('Ctrl Pts',(-14.398022765968,12.3306024799635,8.272244040603));
#6629=CARTESIAN_POINT('Ctrl Pts',(-13.8717069764943,12.5795817775447,11.276975687295));
#6630=CARTESIAN_POINT('Ctrl Pts',(-13.3453911870206,11.3684581001844,14.0380594999119));
#6631=CARTESIAN_POINT('Ctrl Pts',(-12.8190753975469,8.98917609114738,15.8899290067425));
#6632=CARTESIAN_POINT('Ctrl Pts',(-12.2927596080733,6.01526749622851,16.3861865954599));
#6633=CARTESIAN_POINT('Ctrl Pts',(-11.7664438185996,3.1636004708241,15.4072080579704));
#6634=CARTESIAN_POINT('Ctrl Pts',(-11.2401280291259,1.12157644391819,13.1889786533539));
#6635=CARTESIAN_POINT('Ctrl Pts',(-10.7138122396522,0.381430421865054,10.2662081014912));
#6636=CARTESIAN_POINT('Ctrl Pts',(-10.1874964501785,1.1215764447637,7.34343755272727));
#6637=CARTESIAN_POINT('Ctrl Pts',(-9.66118066070484,3.16360046867936,5.12520814334897));
#6638=CARTESIAN_POINT('Ctrl Pts',(-9.13486487123116,6.01526750082342,4.14622961483952));
#6639=CARTESIAN_POINT('Ctrl Pts',(-8.60854908175746,8.98917608163649,4.6424871855396));
#6640=CARTESIAN_POINT('Ctrl Pts',(-8.08223329228379,11.3684581197151,6.49435672909347));
#6641=CARTESIAN_POINT('Ctrl Pts',(-7.55591750281009,12.5795817375133,9.25544046657416));
#6642=CARTESIAN_POINT('Ctrl Pts',(-7.02960171333642,12.330602561978,12.2601722671361));
#6643=CARTESIAN_POINT('Ctrl Pts',(-6.50328592386273,10.6815376452661,14.7842540256155));
#6644=CARTESIAN_POINT('Ctrl Pts',(-5.97697013438905,8.02989820421129,16.2192495300461));
#6645=CARTESIAN_POINT('Ctrl Pts',(-5.45065434491537,5.01486854879121,16.2192495300445));
#6646=CARTESIAN_POINT('Ctrl Pts',(-4.92433855544167,2.36322910773836,14.784254025618));
#6647=CARTESIAN_POINT('Ctrl Pts',(-4.39802276596799,0.714164191021466,12.2601722671314));
#6648=CARTESIAN_POINT('Ctrl Pts',(-3.87170697649431,0.465185015496949,9.25544046658345));
#6649=CARTESIAN_POINT('Ctrl Pts',(-3.34539118702063,1.6763086332728,6.49435672907451));
#6650=CARTESIAN_POINT('Ctrl Pts',(-2.81907539754694,4.0555906713972,4.6424871855784));
#6651=CARTESIAN_POINT('Ctrl Pts',(-2.29275960807326,7.02949925211648,4.14622961476005));
#6652=CARTESIAN_POINT('Ctrl Pts',(-1.76644381859957,9.88116628445271,5.12520814351175));
#6653=CARTESIAN_POINT('Ctrl Pts',(-1.24012802912589,11.9231903079747,7.34343755239381));
#6654=CARTESIAN_POINT('Ctrl Pts',(-0.713812239652205,12.6633363316798,10.2662081021742));
#6655=CARTESIAN_POINT('Ctrl Pts',(-0.187496450178523,11.9231903079747,13.1889786519547));
#6656=CARTESIAN_POINT('Ctrl Pts',(0.338819339295166,9.88116628445271,15.4072080608367));
#6657=CARTESIAN_POINT('Ctrl Pts',(0.865135128768847,7.02949925211648,16.3861865895884));
#6658=CARTESIAN_POINT('Ctrl Pts',(1.39145091824253,4.0555906713972,15.8899290187701));
#6659=CARTESIAN_POINT('Ctrl Pts',(1.91776670771622,1.67630863327279,14.0380594752739));
#6660=CARTESIAN_POINT('Ctrl Pts',(2.4440824971899,0.465185015496951,11.276975737765));
#6661=CARTESIAN_POINT('Ctrl Pts',(2.97039828666358,0.714164191021463,8.27224393721703));
#6662=CARTESIAN_POINT('Ctrl Pts',(3.49671407613727,2.36322910773836,5.74816217873048));
#6663=CARTESIAN_POINT('Ctrl Pts',(4.02302986561095,5.0148685487912,4.31316667430399));
#6664=CARTESIAN_POINT('Ctrl Pts',(4.54934565508464,8.02989820421128,4.3131666743024));
#6665=CARTESIAN_POINT('Ctrl Pts',(5.07566144455832,10.6815376452661,5.74816217873292));
#6666=CARTESIAN_POINT('Ctrl Pts',(5.60197723403201,12.330602561978,8.27224393721239));
#6667=CARTESIAN_POINT('Ctrl Pts',(6.12829302350569,12.5795817375133,11.2769757377743));
#6668=CARTESIAN_POINT('Ctrl Pts',(6.65460881297937,11.3684581197151,14.038059475255));
#6669=CARTESIAN_POINT('Ctrl Pts',(7.18092460245306,8.98917608163649,15.8899290188089));
#6670=CARTESIAN_POINT('Ctrl Pts',(7.70724039192674,6.01526750082342,16.3861865895089));
#6671=CARTESIAN_POINT('Ctrl Pts',(8.23355618140043,3.16360046867936,15.4072080609995));
#6672=CARTESIAN_POINT('Ctrl Pts',(8.75987197087411,1.1215764447637,13.1889786516212));
#6673=CARTESIAN_POINT('Ctrl Pts',(9.28618776034779,0.381430421865052,10.2662081028573));
#6674=CARTESIAN_POINT('Ctrl Pts',(9.81250354982149,1.12157644391819,7.34343755099458));
#6675=CARTESIAN_POINT('Ctrl Pts',(10.3388193392952,3.16360047082409,5.12520814637803));
#6676=CARTESIAN_POINT('Ctrl Pts',(10.8651351287689,6.01526749622852,4.14622960888857));
#6677=CARTESIAN_POINT('Ctrl Pts',(11.3914509182425,8.98917609114738,4.64248719760592));
#6678=CARTESIAN_POINT('Ctrl Pts',(11.9177667077162,11.3684581001844,6.49435670443657));
#6679=CARTESIAN_POINT('Ctrl Pts',(12.4440824971899,12.5795817775447,9.25544051705342));
#6680=CARTESIAN_POINT('Ctrl Pts',(12.9703982866636,12.3306024799635,12.2601721637455));
#6681=CARTESIAN_POINT('Ctrl Pts',(13.4967140761373,10.6815378132754,14.7842542374005));
#6682=CARTESIAN_POINT('Ctrl Pts',(14.023029865611,8.02989786004727,16.2192490962153));
#6683=CARTESIAN_POINT('Ctrl Pts',(14.5493456550846,5.0148692538005,16.21925041873));
#6684=CARTESIAN_POINT('Ctrl Pts',(15.0756614445583,2.36322766355062,14.7842522051773));
#6685=CARTESIAN_POINT('Ctrl Pts',(15.601977234032,0.714167149390356,12.2601759962408));
#6686=CARTESIAN_POINT('Ctrl Pts',(16.1282930235057,0.46517895536534,9.25543282762478));
#6687=CARTESIAN_POINT('Ctrl Pts',(16.6546088129794,1.67632104728413,6.49437237730269));
#6688=CARTESIAN_POINT('Ctrl Pts',(17.1809246024531,4.05556523698548,4.64245512841697));
#6689=CARTESIAN_POINT('Ctrl Pts',(17.7072403919268,7.02955135660707,4.14629530462416));
#6690=CARTESIAN_POINT('Ctrl Pts',(18.2335561814004,9.8810581004343,5.12507291707035));
#6691=CARTESIAN_POINT('Ctrl Pts',(18.7598719708741,11.9234097510006,7.34371986926018));
#6692=CARTESIAN_POINT('Ctrl Pts',(19.1107491638566,12.4160945610234,9.29153159762474));
#6693=CARTESIAN_POINT('Ctrl Pts',(19.2861877603478,12.4160945610234,10.2662081021742));
#6694=CARTESIAN_POINT('Ctrl Pts',(-21.,11.8215826768434,10.2662081021742));
#6695=CARTESIAN_POINT('Ctrl Pts',(-20.8245614035088,11.8215826768434,11.1423372082236));
#6696=CARTESIAN_POINT('Ctrl Pts',(-20.4736842105263,11.3785434349997,12.8940021805135));
#6697=CARTESIAN_POINT('Ctrl Pts',(-19.9473684210526,9.54224664734747,14.8886522715445));
#6698=CARTESIAN_POINT('Ctrl Pts',(-19.421052631579,6.9783848758886,15.7687789642738));
#6699=CARTESIAN_POINT('Ctrl Pts',(-18.8947368421052,4.30441716130508,15.322628929525));
#6700=CARTESIAN_POINT('Ctrl Pts',(-18.3684210526316,2.16518578050098,13.6575517805422));
#6701=CARTESIAN_POINT('Ctrl Pts',(-17.8421052631579,1.07622381336149,11.1750141268389));
#6702=CARTESIAN_POINT('Ctrl Pts',(-17.3157894736842,1.30009366399148,8.47339120268354));
#6703=CARTESIAN_POINT('Ctrl Pts',(-16.7894736842105,2.78279902034384,6.20393874295387));
#6704=CARTESIAN_POINT('Ctrl Pts',(-16.2631578947368,5.16694563809232,4.91370280999657));
#6705=CARTESIAN_POINT('Ctrl Pts',(-15.7368421052632,7.87782141228263,4.91370342697971));
#6706=CARTESIAN_POINT('Ctrl Pts',(-15.2105263157895,10.2619666809626,6.20393779487563));
#6707=CARTESIAN_POINT('Ctrl Pts',(-14.6842105263158,11.7446754594104,8.47339299062945));
#6708=CARTESIAN_POINT('Ctrl Pts',(-14.1578947368421,11.9685379784868,11.1750105395485));
#6709=CARTESIAN_POINT('Ctrl Pts',(-13.6315789473684,10.8795911867729,13.6575590922666));
#6710=CARTESIAN_POINT('Ctrl Pts',(-13.1052631578947,8.74032863907908,15.3226139692546));
#6711=CARTESIAN_POINT('Ctrl Pts',(-12.5789473684211,6.06642481255227,15.7688096072721));
#6712=CARTESIAN_POINT('Ctrl Pts',(-12.0526315789474,3.50243095315069,14.8885893974933));
#6713=CARTESIAN_POINT('Ctrl Pts',(-11.5263157894737,1.66640415994231,12.8941326374224));
#6714=CARTESIAN_POINT('Ctrl Pts',(-11.,1.0009232890457,10.2662081018556));
#6715=CARTESIAN_POINT('Ctrl Pts',(-10.4736842105263,1.66640416063908,7.63828356773443));
#6716=CARTESIAN_POINT('Ctrl Pts',(-9.94736842105264,3.50243095138322,5.64382680544198));
#6717=CARTESIAN_POINT('Ctrl Pts',(-9.42105263157895,6.06642481633893,4.7636065998526));
#6718=CARTESIAN_POINT('Ctrl Pts',(-8.89473684210527,8.74032863124119,5.20980222946469));
#6719=CARTESIAN_POINT('Ctrl Pts',(-8.36842105263158,10.8795912028682,6.87485712358485));
#6720=CARTESIAN_POINT('Ctrl Pts',(-7.84210526315789,11.968537945497,9.35740564125021));
#6721=CARTESIAN_POINT('Ctrl Pts',(-7.31578947368422,11.7446755269984,12.0590232619531));
#6722=CARTESIAN_POINT('Ctrl Pts',(-6.78947368421053,10.2619665425062,14.3284783106703));
#6723=CARTESIAN_POINT('Ctrl Pts',(-6.26315789473684,7.87782169590793,15.6187129797607));
#6724=CARTESIAN_POINT('Ctrl Pts',(-5.73684210526316,5.16694505709463,15.6187129797599));
#6725=CARTESIAN_POINT('Ctrl Pts',(-5.21052631578947,2.782800210498,14.3284783106715));
#6726=CARTESIAN_POINT('Ctrl Pts',(-4.68421052631579,1.30009122600162,12.0590232619509));
#6727=CARTESIAN_POINT('Ctrl Pts',(-4.15789473684211,1.07622880751197,9.35740564125455));
#6728=CARTESIAN_POINT('Ctrl Pts',(-3.63157894736843,2.16517555012239,6.87485712357599));
#6729=CARTESIAN_POINT('Ctrl Pts',(-3.10526315789474,4.30443812178711,5.20980222948279));
#6730=CARTESIAN_POINT('Ctrl Pts',(-2.57894736842106,6.97834193661205,4.76360659981552));
#6731=CARTESIAN_POINT('Ctrl Pts',(-2.05263157894737,9.54233580172614,5.64382680551793));
#6732=CARTESIAN_POINT('Ctrl Pts',(-1.52631578947369,11.3783625921458,7.63828356757886));
#6733=CARTESIAN_POINT('Ctrl Pts',(-1.,12.0438434644038,10.2662081021742));
#6734=CARTESIAN_POINT('Ctrl Pts',(-0.47368421052632,11.3783625921459,12.8941326367696));
#6735=CARTESIAN_POINT('Ctrl Pts',(0.0526315789473631,9.54233580172614,14.8885893988306));
#6736=CARTESIAN_POINT('Ctrl Pts',(0.578947368421052,6.97834193661205,15.7688096045329));
#6737=CARTESIAN_POINT('Ctrl Pts',(1.10526315789473,4.3044381217871,15.3226139748657));
#6738=CARTESIAN_POINT('Ctrl Pts',(1.63157894736842,2.16517555012238,13.6575590807725));
#6739=CARTESIAN_POINT('Ctrl Pts',(2.1578947368421,1.07622880751197,11.1750105630939));
#6740=CARTESIAN_POINT('Ctrl Pts',(2.68421052631579,1.30009122600162,8.47339294239756));
#6741=CARTESIAN_POINT('Ctrl Pts',(3.21052631578947,2.782800210498,6.203937893677));
#6742=CARTESIAN_POINT('Ctrl Pts',(3.73684210526315,5.16694505709462,4.91370322458856));
#6743=CARTESIAN_POINT('Ctrl Pts',(4.26315789473684,7.87782169590794,4.91370322458781));
#6744=CARTESIAN_POINT('Ctrl Pts',(4.78947368421052,10.2619665425062,6.20393789367814));
#6745=CARTESIAN_POINT('Ctrl Pts',(5.31578947368421,11.7446755269984,8.47339294239539));
#6746=CARTESIAN_POINT('Ctrl Pts',(5.84210526315788,11.968537945497,11.1750105630982));
#6747=CARTESIAN_POINT('Ctrl Pts',(6.36842105263158,10.8795912028682,13.6575590807636));
#6748=CARTESIAN_POINT('Ctrl Pts',(6.89473684210526,8.74032863124118,15.3226139748838));
#6749=CARTESIAN_POINT('Ctrl Pts',(7.42105263157895,6.06642481633893,15.7688096044959));
#6750=CARTESIAN_POINT('Ctrl Pts',(7.94736842105263,3.50243095138322,14.8885893989065));
#6751=CARTESIAN_POINT('Ctrl Pts',(8.47368421052631,1.66640416063909,12.894132636614));
#6752=CARTESIAN_POINT('Ctrl Pts',(9.,1.0009232890457,10.2662081024929));
#6753=CARTESIAN_POINT('Ctrl Pts',(9.52631578947368,1.66640415994231,7.63828356692609));
#6754=CARTESIAN_POINT('Ctrl Pts',(10.0526315789474,3.50243095315069,5.64382680685511));
#6755=CARTESIAN_POINT('Ctrl Pts',(10.578947368421,6.06642481255228,4.76360659707634));
#6756=CARTESIAN_POINT('Ctrl Pts',(11.1052631578947,8.74032863907909,5.20980223509391));
#6757=CARTESIAN_POINT('Ctrl Pts',(11.6315789473684,10.8795911867729,6.87485711208184));
#6758=CARTESIAN_POINT('Ctrl Pts',(12.1578947368421,11.9685379784868,9.35740566479993));
#6759=CARTESIAN_POINT('Ctrl Pts',(12.6842105263158,11.7446754594104,12.059023213719));
#6760=CARTESIAN_POINT('Ctrl Pts',(13.2105263157895,10.2619666809626,14.3284784094728));
#6761=CARTESIAN_POINT('Ctrl Pts',(13.7368421052632,7.8778214122826,15.6187127773688));
#6762=CARTESIAN_POINT('Ctrl Pts',(14.2631578947369,5.16694563809232,15.6187133943519));
#6763=CARTESIAN_POINT('Ctrl Pts',(14.7894736842105,2.78279902034383,14.3284774613946));
#6764=CARTESIAN_POINT('Ctrl Pts',(15.3157894736842,1.30009366399149,12.0590250016649));
#6765=CARTESIAN_POINT('Ctrl Pts',(15.8421052631579,1.07622381336148,9.3574020775096));
#6766=CARTESIAN_POINT('Ctrl Pts',(16.3684210526316,2.16518578050099,6.87486442380621));
#6767=CARTESIAN_POINT('Ctrl Pts',(16.8947368421052,4.30441716130507,5.2097872748235));
#6768=CARTESIAN_POINT('Ctrl Pts',(17.421052631579,6.9783848758886,4.76363724007471));
#6769=CARTESIAN_POINT('Ctrl Pts',(17.9473684210526,9.54224664734746,5.64376393280394));
#6770=CARTESIAN_POINT('Ctrl Pts',(18.4736842105263,11.3785434349997,7.63841402383501));
#6771=CARTESIAN_POINT('Ctrl Pts',(18.8245614035088,11.8215826768433,9.39007899612484));
#6772=CARTESIAN_POINT('Ctrl Pts',(19.,11.8215826768434,10.2662081021742));
#6773=CARTESIAN_POINT('Ctrl Pts',(-21.,11.5223833765015,10.2662081021742));
#6774=CARTESIAN_POINT('Ctrl Pts',(-20.8245614035088,11.5223833765015,11.0929430110137));
#6775=CARTESIAN_POINT('Ctrl Pts',(-20.4736842105263,11.1043754458166,12.7456006386873));
#6776=CARTESIAN_POINT('Ctrl Pts',(-19.9473684210526,9.37174604195822,14.627693070812));
#6777=CARTESIAN_POINT('Ctrl Pts',(-19.421052631579,6.95264079877442,15.4581010648004));
#6778=CARTESIAN_POINT('Ctrl Pts',(-18.8947368421052,4.4296403847971,15.0371536204255));
#6779=CARTESIAN_POINT('Ctrl Pts',(-18.3684210526316,2.41118846113653,13.4660782459265));
#6780=CARTESIAN_POINT('Ctrl Pts',(-17.8421052631579,1.38370759752575,11.1237050325294));
#6781=CARTESIAN_POINT('Ctrl Pts',(-17.3157894736842,1.59493822839275,8.57461107686665));
#6782=CARTESIAN_POINT('Ctrl Pts',(-16.7894736842105,2.9939316339387,6.43329006745293));
#6783=CARTESIAN_POINT('Ctrl Pts',(-16.2631578947368,5.2434721166514,5.21589900368628));
#6784=CARTESIAN_POINT('Ctrl Pts',(-15.7368421052632,7.80129492555693,5.21589976806491));
#6785=CARTESIAN_POINT('Ctrl Pts',(-15.2105263157895,10.0508340962501,6.43328889288153));
#6786=CARTESIAN_POINT('Ctrl Pts',(-14.6842105263158,11.4498308299117,8.57461329194773));
#6787=CARTESIAN_POINT('Ctrl Pts',(-14.1578947368421,11.6610543305691,11.1237005882441));
#6788=CARTESIAN_POINT('Ctrl Pts',(-13.6315789473684,10.6335882256263,13.4660873044149));
#6789=CARTESIAN_POINT('Ctrl Pts',(-13.1052631578947,8.61510599100168,15.0371350857393));
#6790=CARTESIAN_POINT('Ctrl Pts',(-12.5789473684211,6.09216771054517,15.4581390317312));
#6791=CARTESIAN_POINT('Ctrl Pts',(-12.0526315789474,3.67293400690476,14.6276150452767));
#6792=CARTESIAN_POINT('Ctrl Pts',(-11.5263157894737,1.94056718272496,12.7457630293102));
#6793=CARTESIAN_POINT('Ctrl Pts',(-11.,1.31265859936127,10.2662081017794));
#6794=CARTESIAN_POINT('Ctrl Pts',(-10.4736842105263,1.9405671834026,7.78665317603972));
#6795=CARTESIAN_POINT('Ctrl Pts',(-9.94736842105264,3.67293400518582,5.90480115732107));
#6796=CARTESIAN_POINT('Ctrl Pts',(-9.42105263157895,6.09216771422783,5.07427717605678));
#6797=CARTESIAN_POINT('Ctrl Pts',(-8.89473684210527,8.61510598337903,5.49528111163513));
#6798=CARTESIAN_POINT('Ctrl Pts',(-8.36842105263158,10.6335882412796,7.06632891418456));
#6799=CARTESIAN_POINT('Ctrl Pts',(-7.84210526315789,11.6610542984852,9.40871558692863));
#6800=CARTESIAN_POINT('Ctrl Pts',(-7.31578947368422,11.4498308956436,11.9578029721578));
#6801=CARTESIAN_POINT('Ctrl Pts',(-6.78947368421053,10.0508339615961,14.0991271890608));
#6802=CARTESIAN_POINT('Ctrl Pts',(-6.26315789473684,7.80129520139315,15.3165166870263));
#6803=CARTESIAN_POINT('Ctrl Pts',(-5.73684210526316,5.24347155160944,15.3165166870254));
#6804=CARTESIAN_POINT('Ctrl Pts',(-5.21052631578947,2.99393279140807,14.0991271890622));
#6805=CARTESIAN_POINT('Ctrl Pts',(-4.68421052631579,1.59493585735657,11.9578029721551));
#6806=CARTESIAN_POINT('Ctrl Pts',(-4.15789473684211,1.38371245452358,9.408715586934));
#6807=CARTESIAN_POINT('Ctrl Pts',(-3.63157894736843,2.41117851171133,7.0663289141736));
#6808=CARTESIAN_POINT('Ctrl Pts',(-3.10526315789474,4.42966076964857,5.49528111165755));
#6809=CARTESIAN_POINT('Ctrl Pts',(-2.57894736842106,6.95259903872457,5.07427717601085));
#6810=CARTESIAN_POINT('Ctrl Pts',(-2.05263157894737,9.3718327479206,5.90480115741515));
#6811=CARTESIAN_POINT('Ctrl Pts',(-1.52631578947369,11.1041995693883,7.78665317584699));
#6812=CARTESIAN_POINT('Ctrl Pts',(-1.,11.732108154076,10.2662081021742));
#6813=CARTESIAN_POINT('Ctrl Pts',(-0.47368421052632,11.1041995693883,12.7457630285015));
#6814=CARTESIAN_POINT('Ctrl Pts',(0.052631578947363,9.37183274792061,14.6276150469333));
#6815=CARTESIAN_POINT('Ctrl Pts',(0.578947368421052,6.95259903872456,15.4581390283376));
#6816=CARTESIAN_POINT('Ctrl Pts',(1.10526315789473,4.42966076964857,15.0371350926909));
#6817=CARTESIAN_POINT('Ctrl Pts',(1.63157894736842,2.41117851171132,13.4660872901749));
#6818=CARTESIAN_POINT('Ctrl Pts',(2.1578947368421,1.38371245452358,11.1237006174145));
#6819=CARTESIAN_POINT('Ctrl Pts',(2.68421052631579,1.59493585735657,8.57461323219337));
#6820=CARTESIAN_POINT('Ctrl Pts',(3.21052631578947,2.99393279140808,6.43328901528626));
#6821=CARTESIAN_POINT('Ctrl Pts',(3.73684210526315,5.24347155160942,5.21589951732309));
#6822=CARTESIAN_POINT('Ctrl Pts',(4.26315789473684,7.80129520139315,5.21589951732216));
#6823=CARTESIAN_POINT('Ctrl Pts',(4.78947368421052,10.0508339615961,6.43328901528768));
#6824=CARTESIAN_POINT('Ctrl Pts',(5.31578947368421,11.4498308956436,8.57461323219068));
#6825=CARTESIAN_POINT('Ctrl Pts',(5.84210526315788,11.6610542984852,11.1237006174198));
#6826=CARTESIAN_POINT('Ctrl Pts',(6.36842105263158,10.6335882412796,13.4660872901639));
#6827=CARTESIAN_POINT('Ctrl Pts',(6.89473684210526,8.61510598337902,15.0371350927133));
#6828=CARTESIAN_POINT('Ctrl Pts',(7.42105263157895,6.09216771422785,15.4581390282917));
#6829=CARTESIAN_POINT('Ctrl Pts',(7.94736842105263,3.67293400518582,14.6276150470274));
#6830=CARTESIAN_POINT('Ctrl Pts',(8.47368421052631,1.94056718340261,12.7457630283087));
#6831=CARTESIAN_POINT('Ctrl Pts',(9.,1.31265859936126,10.266208102569));
#6832=CARTESIAN_POINT('Ctrl Pts',(9.52631578947368,1.94056718272496,7.78665317503828));
#6833=CARTESIAN_POINT('Ctrl Pts',(10.0526315789474,3.67293400690476,5.90480115907178));
#6834=CARTESIAN_POINT('Ctrl Pts',(10.578947368421,6.09216771054518,5.07427717261729));
#6835=CARTESIAN_POINT('Ctrl Pts',(11.1052631578947,8.61510599100168,5.49528111860915));
#6836=CARTESIAN_POINT('Ctrl Pts',(11.6315789473684,10.6335882256264,7.06632889993352));
#6837=CARTESIAN_POINT('Ctrl Pts',(12.1578947368421,11.6610543305691,9.40871561610432));
#6838=CARTESIAN_POINT('Ctrl Pts',(12.6842105263158,11.4498308299117,11.9578029124007));
#6839=CARTESIAN_POINT('Ctrl Pts',(13.2105263157895,10.0508340962501,14.0991273114669));
#6840=CARTESIAN_POINT('Ctrl Pts',(13.7368421052632,7.80129492555691,15.3165164362836));
#6841=CARTESIAN_POINT('Ctrl Pts',(14.2631578947369,5.24347211665139,15.3165172006622));
#6842=CARTESIAN_POINT('Ctrl Pts',(14.7894736842105,2.9939316339387,14.0991261368955));
#6843=CARTESIAN_POINT('Ctrl Pts',(15.3157894736842,1.59493822839275,11.9578051274818));
#6844=CARTESIAN_POINT('Ctrl Pts',(15.8421052631579,1.38370759752574,9.4087111718191));
#6845=CARTESIAN_POINT('Ctrl Pts',(16.3684210526316,2.41118846113653,7.06633795842197));
#6846=CARTESIAN_POINT('Ctrl Pts',(16.8947368421052,4.42964038479711,5.49526258392294));
#6847=CARTESIAN_POINT('Ctrl Pts',(17.421052631579,6.95264079877441,5.07431513954803));
#6848=CARTESIAN_POINT('Ctrl Pts',(17.9473684210526,9.37174604195823,5.90472313353644));
#6849=CARTESIAN_POINT('Ctrl Pts',(18.4736842105263,11.1043754458165,7.78681556566119));
#6850=CARTESIAN_POINT('Ctrl Pts',(18.8245614035088,11.5223833765015,9.43947319333481));
#6851=CARTESIAN_POINT('Ctrl Pts',(19.,11.5223833765015,10.2662081021742));
#6852=CARTESIAN_POINT('',(-21.,11.5223833765015,10.2662081021742));
#6853=CARTESIAN_POINT('Origin',(-20.,11.5223833765015,10.2662081021742));
#6854=CARTESIAN_POINT('',(19.,11.5223833765015,10.2662081021742));
#6855=CARTESIAN_POINT('Ctrl Pts',(-21.,11.5223833765015,10.2662081021742));
#6856=CARTESIAN_POINT('Ctrl Pts',(-20.8245614035088,11.5223833765015,11.0929430110137));
#6857=CARTESIAN_POINT('Ctrl Pts',(-20.4736842105263,11.1043754458166,12.7456006386873));
#6858=CARTESIAN_POINT('Ctrl Pts',(-19.9473684210526,9.37174604195822,14.627693070812));
#6859=CARTESIAN_POINT('Ctrl Pts',(-19.421052631579,6.95264079877442,15.4581010648004));
#6860=CARTESIAN_POINT('Ctrl Pts',(-18.8947368421052,4.4296403847971,15.0371536204255));
#6861=CARTESIAN_POINT('Ctrl Pts',(-18.3684210526316,2.41118846113653,13.4660782459265));
#6862=CARTESIAN_POINT('Ctrl Pts',(-17.8421052631579,1.38370759752575,11.1237050325294));
#6863=CARTESIAN_POINT('Ctrl Pts',(-17.3157894736842,1.59493822839275,8.57461107686665));
#6864=CARTESIAN_POINT('Ctrl Pts',(-16.7894736842105,2.9939316339387,6.43329006745293));
#6865=CARTESIAN_POINT('Ctrl Pts',(-16.2631578947368,5.2434721166514,5.21589900368628));
#6866=CARTESIAN_POINT('Ctrl Pts',(-15.7368421052632,7.80129492555693,5.21589976806491));
#6867=CARTESIAN_POINT('Ctrl Pts',(-15.2105263157895,10.0508340962501,6.43328889288153));
#6868=CARTESIAN_POINT('Ctrl Pts',(-14.6842105263158,11.4498308299117,8.57461329194773));
#6869=CARTESIAN_POINT('Ctrl Pts',(-14.1578947368421,11.6610543305691,11.1237005882441));
#6870=CARTESIAN_POINT('Ctrl Pts',(-13.6315789473684,10.6335882256263,13.4660873044149));
#6871=CARTESIAN_POINT('Ctrl Pts',(-13.1052631578947,8.61510599100168,15.0371350857393));
#6872=CARTESIAN_POINT('Ctrl Pts',(-12.5789473684211,6.09216771054517,15.4581390317312));
#6873=CARTESIAN_POINT('Ctrl Pts',(-12.0526315789474,3.67293400690476,14.6276150452767));
#6874=CARTESIAN_POINT('Ctrl Pts',(-11.5263157894737,1.94056718272496,12.7457630293102));
#6875=CARTESIAN_POINT('Ctrl Pts',(-11.,1.31265859936127,10.2662081017794));
#6876=CARTESIAN_POINT('Ctrl Pts',(-10.4736842105263,1.9405671834026,7.78665317603972));
#6877=CARTESIAN_POINT('Ctrl Pts',(-9.94736842105264,3.67293400518582,5.90480115732107));
#6878=CARTESIAN_POINT('Ctrl Pts',(-9.42105263157895,6.09216771422783,5.07427717605678));
#6879=CARTESIAN_POINT('Ctrl Pts',(-8.89473684210527,8.61510598337903,5.49528111163513));
#6880=CARTESIAN_POINT('Ctrl Pts',(-8.36842105263158,10.6335882412796,7.06632891418456));
#6881=CARTESIAN_POINT('Ctrl Pts',(-7.84210526315789,11.6610542984852,9.40871558692863));
#6882=CARTESIAN_POINT('Ctrl Pts',(-7.31578947368422,11.4498308956436,11.9578029721578));
#6883=CARTESIAN_POINT('Ctrl Pts',(-6.78947368421053,10.0508339615961,14.0991271890608));
#6884=CARTESIAN_POINT('Ctrl Pts',(-6.26315789473684,7.80129520139315,15.3165166870263));
#6885=CARTESIAN_POINT('Ctrl Pts',(-5.73684210526316,5.24347155160944,15.3165166870254));
#6886=CARTESIAN_POINT('Ctrl Pts',(-5.21052631578947,2.99393279140807,14.0991271890622));
#6887=CARTESIAN_POINT('Ctrl Pts',(-4.68421052631579,1.59493585735657,11.9578029721551));
#6888=CARTESIAN_POINT('Ctrl Pts',(-4.15789473684211,1.38371245452358,9.408715586934));
#6889=CARTESIAN_POINT('Ctrl Pts',(-3.63157894736843,2.41117851171133,7.0663289141736));
#6890=CARTESIAN_POINT('Ctrl Pts',(-3.10526315789474,4.42966076964857,5.49528111165755));
#6891=CARTESIAN_POINT('Ctrl Pts',(-2.57894736842106,6.95259903872457,5.07427717601085));
#6892=CARTESIAN_POINT('Ctrl Pts',(-2.05263157894737,9.3718327479206,5.90480115741515));
#6893=CARTESIAN_POINT('Ctrl Pts',(-1.52631578947369,11.1041995693883,7.78665317584699));
#6894=CARTESIAN_POINT('Ctrl Pts',(-1.,11.732108154076,10.2662081021742));
#6895=CARTESIAN_POINT('Ctrl Pts',(-0.47368421052632,11.1041995693883,12.7457630285015));
#6896=CARTESIAN_POINT('Ctrl Pts',(0.052631578947363,9.37183274792061,14.6276150469333));
#6897=CARTESIAN_POINT('Ctrl Pts',(0.578947368421052,6.95259903872456,15.4581390283376));
#6898=CARTESIAN_POINT('Ctrl Pts',(1.10526315789473,4.42966076964857,15.0371350926909));
#6899=CARTESIAN_POINT('Ctrl Pts',(1.63157894736842,2.41117851171132,13.4660872901749));
#6900=CARTESIAN_POINT('Ctrl Pts',(2.1578947368421,1.38371245452358,11.1237006174145));
#6901=CARTESIAN_POINT('Ctrl Pts',(2.68421052631579,1.59493585735657,8.57461323219337));
#6902=CARTESIAN_POINT('Ctrl Pts',(3.21052631578947,2.99393279140808,6.43328901528626));
#6903=CARTESIAN_POINT('Ctrl Pts',(3.73684210526315,5.24347155160942,5.21589951732309));
#6904=CARTESIAN_POINT('Ctrl Pts',(4.26315789473684,7.80129520139315,5.21589951732216));
#6905=CARTESIAN_POINT('Ctrl Pts',(4.78947368421052,10.0508339615961,6.43328901528768));
#6906=CARTESIAN_POINT('Ctrl Pts',(5.31578947368421,11.4498308956436,8.57461323219068));
#6907=CARTESIAN_POINT('Ctrl Pts',(5.84210526315788,11.6610542984852,11.1237006174198));
#6908=CARTESIAN_POINT('Ctrl Pts',(6.36842105263158,10.6335882412796,13.4660872901639));
#6909=CARTESIAN_POINT('Ctrl Pts',(6.89473684210526,8.61510598337902,15.0371350927133));
#6910=CARTESIAN_POINT('Ctrl Pts',(7.42105263157895,6.09216771422785,15.4581390282917));
#6911=CARTESIAN_POINT('Ctrl Pts',(7.94736842105263,3.67293400518582,14.6276150470274));
#6912=CARTESIAN_POINT('Ctrl Pts',(8.47368421052631,1.94056718340261,12.7457630283087));
#6913=CARTESIAN_POINT('Ctrl Pts',(9.,1.31265859936126,10.266208102569));
#6914=CARTESIAN_POINT('Ctrl Pts',(9.52631578947368,1.94056718272496,7.78665317503828));
#6915=CARTESIAN_POINT('Ctrl Pts',(10.0526315789474,3.67293400690476,5.90480115907178));
#6916=CARTESIAN_POINT('Ctrl Pts',(10.578947368421,6.09216771054518,5.07427717261729));
#6917=CARTESIAN_POINT('Ctrl Pts',(11.1052631578947,8.61510599100168,5.49528111860915));
#6918=CARTESIAN_POINT('Ctrl Pts',(11.6315789473684,10.6335882256264,7.06632889993352));
#6919=CARTESIAN_POINT('Ctrl Pts',(12.1578947368421,11.6610543305691,9.40871561610432));
#6920=CARTESIAN_POINT('Ctrl Pts',(12.6842105263158,11.4498308299117,11.9578029124007));
#6921=CARTESIAN_POINT('Ctrl Pts',(13.2105263157895,10.0508340962501,14.0991273114669));
#6922=CARTESIAN_POINT('Ctrl Pts',(13.7368421052632,7.80129492555691,15.3165164362836));
#6923=CARTESIAN_POINT('Ctrl Pts',(14.2631578947369,5.24347211665139,15.3165172006622));
#6924=CARTESIAN_POINT('Ctrl Pts',(14.7894736842105,2.9939316339387,14.0991261368955));
#6925=CARTESIAN_POINT('Ctrl Pts',(15.3157894736842,1.59493822839275,11.9578051274818));
#6926=CARTESIAN_POINT('Ctrl Pts',(15.8421052631579,1.38370759752574,9.4087111718191));
#6927=CARTESIAN_POINT('Ctrl Pts',(16.3684210526316,2.41118846113653,7.06633795842197));
#6928=CARTESIAN_POINT('Ctrl Pts',(16.8947368421052,4.42964038479711,5.49526258392294));
#6929=CARTESIAN_POINT('Ctrl Pts',(17.421052631579,6.95264079877441,5.07431513954803));
#6930=CARTESIAN_POINT('Ctrl Pts',(17.9473684210526,9.37174604195823,5.90472313353644));
#6931=CARTESIAN_POINT('Ctrl Pts',(18.4736842105263,11.1043754458165,7.78681556566119));
#6932=CARTESIAN_POINT('Ctrl Pts',(18.8245614035088,11.5223833765015,9.43947319333481));
#6933=CARTESIAN_POINT('Ctrl Pts',(19.,11.5223833765015,10.2662081021742));
#6934=CARTESIAN_POINT('Origin',(20.,11.5223833765015,10.2662081021742));
#6935=CARTESIAN_POINT('Origin',(20.,11.5223833765015,10.2662081021742));
#6936=CARTESIAN_POINT('Origin',(-20.,11.5223833765015,10.2662081021742));
#7033=UNCERTAINTY_MEASURE_WITH_UNIT(LENGTH_MEASURE(0.01),#7048,
'DISTANCE_ACCURACY_VALUE',
'Maximum model space distance between geometric entities at asserted c
onnectivities');
#7035=UNCERTAINTY_MEASURE_WITH_UNIT(LENGTH_MEASURE(0.01),#7048,
'DISTANCE_ACCURACY_VALUE',
'Maximum model space distance between geometric entities at asserted c
onnectivities');
#7045=(
GEOMETRIC_REPRESENTATION_CONTEXT(3)
GLOBAL_UNCERTAINTY_ASSIGNED_CONTEXT((#7033))
GLOBAL_UNIT_ASSIGNED_CONTEXT((#7048,#7050,#7051))
REPRESENTATION_CONTEXT('','3D')
);
#7047=(
GEOMETRIC_REPRESENTATION_CONTEXT(3)
GLOBAL_UNCERTAINTY_ASSIGNED_CONTEXT((#7035))
GLOBAL_UNIT_ASSIGNED_CONTEXT((#7048,#7050,#7051))
REPRESENTATION_CONTEXT('','3D')
);
#7048=(
LENGTH_UNIT()
NAMED_UNIT(*)
SI_UNIT(.MILLI.,.METRE.)
);
#7050=(
NAMED_UNIT(*)
PLANE_ANGLE_UNIT()
SI_UNIT($,.RADIAN.)
);
#7051=(
NAMED_UNIT(*)
SI_UNIT($,.STERADIAN.)
SOLID_ANGLE_UNIT()
);
#7061=SHAPE_DEFINITION_REPRESENTATION(#7072,#7093);
#7072=PRODUCT_DEFINITION_SHAPE('',$,#7105);
#7093=SHAPE_REPRESENTATION('',(#3860),#7045);
#7095=PRODUCT_DEFINITION_CONTEXT('part definition',#7130,'design');
#7105=PRODUCT_DEFINITION('Spring','Spring',#7116,#7095);
#7116=PRODUCT_DEFINITION_FORMATION('',$,#7141);
#7130=APPLICATION_CONTEXT(
'Core Data for Automotive Mechanical Design Process');
#7131=PRODUCT_CONTEXT('part definition',#7130,'mechanical');
#7141=PRODUCT('Spring','Spring',$,(#7131));
#7192=COLOUR_RGB('Grey',0.48,0.52,0.57);
#7193=FILL_AREA_STYLE_COLOUR('',#7192);
#7194=FILL_AREA_STYLE('',(#7193));
#7195=SURFACE_STYLE_FILL_AREA(#7194);
#7196=SURFACE_SIDE_STYLE('',(#7195));
#7197=SURFACE_STYLE_USAGE(.BOTH.,#7196);
#7198=PRESENTATION_STYLE_ASSIGNMENT((#7197));
ENDSEC;
END-ISO-10303-21;
